ISO-10303-21;
HEADER;
/* Generated by software containing ST-Developer
 * from STEP Tools, Inc. (www.steptools.com) 
 */

FILE_DESCRIPTION(
/* description */ ('Independent maintained push-to-latch/pull-to-reset mushroom-operator 
CAD. Two opposed spring-loaded ball detents in turned circular seats b
ias both travel stops; direct normally-closed bridge opens6mm when pre
ssed. Rounded palm/pull rim, captured head screw, removable detent clo
sures, native Coil spring families, insulated shared terminals and ord
inary machining features. Manual geometric states and ideal same-mater
ial spring-energy direction only; no electrical/safety certification, 
force/contact dynamics, wear, load or life rating. Requested blue/gray
 visual palette, not safety identification. External wiring/anchors an
d application engineering omitted.'),
/* implementation_level */ '2;1');

FILE_NAME(
/* name */ 'Socket head cap screw M3x6.step',
/* time_stamp */ '2026-11-08T17:54:26-08:00',
/* author */ (''),
/* organization */ (''),
/* preprocessor_version */ 'ST-DEVELOPER v20.2',
/* originating_system */ 'Autodesk Translation Framework v15.17.0.0',
/* authorisation */ '');

FILE_SCHEMA (('AUTOMOTIVE_DESIGN { 1 0 10303 214 3 1 1 }'));
ENDSEC;

DATA;
#10=MECHANICAL_DESIGN_GEOMETRIC_PRESENTATION_REPRESENTATION('',(#204),#43980);
#148=CONICAL_SURFACE('',#12130,0.1,0.785398163397448);
#170=SHAPE_REPRESENTATION_RELATIONSHIP('SRR','None',#44070,#187);
#187=ADVANCED_BREP_SHAPE_REPRESENTATION('',(#221),#43977);
#204=STYLED_ITEM('',(#44160),#221);
#221=MANIFOLD_SOLID_BREP('Body1',#11245);
#252=B_SPLINE_SURFACE_WITH_KNOTS('',3,3,((#39668,#39669,#39670,#39671,#39672,
#39673,#39674,#39675,#39676,#39677,#39678,#39679,#39680,#39681,#39682,#39683,
#39684,#39685,#39686,#39687,#39688,#39689,#39690,#39691,#39692,#39693,#39694,
#39695,#39696,#39697,#39698,#39699,#39700,#39701,#39702,#39703,#39704,#39705,
#39706,#39707,#39708,#39709,#39710,#39711,#39712,#39713,#39714,#39715,#39716,
#39717,#39718,#39719,#39720,#39721,#39722,#39723,#39724,#39725,#39726,#39727,
#39728,#39729,#39730,#39731,#39732,#39733,#39734,#39735,#39736,#39737),
(#39738,#39739,#39740,#39741,#39742,#39743,#39744,#39745,#39746,#39747,
#39748,#39749,#39750,#39751,#39752,#39753,#39754,#39755,#39756,#39757,#39758,
#39759,#39760,#39761,#39762,#39763,#39764,#39765,#39766,#39767,#39768,#39769,
#39770,#39771,#39772,#39773,#39774,#39775,#39776,#39777,#39778,#39779,#39780,
#39781,#39782,#39783,#39784,#39785,#39786,#39787,#39788,#39789,#39790,#39791,
#39792,#39793,#39794,#39795,#39796,#39797,#39798,#39799,#39800,#39801,#39802,
#39803,#39804,#39805,#39806,#39807),(#39808,#39809,#39810,#39811,#39812,
#39813,#39814,#39815,#39816,#39817,#39818,#39819,#39820,#39821,#39822,#39823,
#39824,#39825,#39826,#39827,#39828,#39829,#39830,#39831,#39832,#39833,#39834,
#39835,#39836,#39837,#39838,#39839,#39840,#39841,#39842,#39843,#39844,#39845,
#39846,#39847,#39848,#39849,#39850,#39851,#39852,#39853,#39854,#39855,#39856,
#39857,#39858,#39859,#39860,#39861,#39862,#39863,#39864,#39865,#39866,#39867,
#39868,#39869,#39870,#39871,#39872,#39873,#39874,#39875,#39876,#39877),
(#39878,#39879,#39880,#39881,#39882,#39883,#39884,#39885,#39886,#39887,
#39888,#39889,#39890,#39891,#39892,#39893,#39894,#39895,#39896,#39897,#39898,
#39899,#39900,#39901,#39902,#39903,#39904,#39905,#39906,#39907,#39908,#39909,
#39910,#39911,#39912,#39913,#39914,#39915,#39916,#39917,#39918,#39919,#39920,
#39921,#39922,#39923,#39924,#39925,#39926,#39927,#39928,#39929,#39930,#39931,
#39932,#39933,#39934,#39935,#39936,#39937,#39938,#39939,#39940,#39941,#39942,
#39943,#39944,#39945,#39946,#39947)),.UNSPECIFIED.,.F.,.F.,.F.,(4,4),(4,
1,1,1,1,1,1,1,1,1,1,1,1,1,1,1,1,1,1,1,1,1,1,1,1,1,1,1,1,1,1,1,1,1,1,1,1,
1,1,1,1,1,1,1,1,1,1,1,1,1,1,1,1,1,1,1,1,1,1,1,1,1,1,1,1,1,1,4),(0.,0.0329955678841871),
(11.6159397475004,12.6141690908179,13.6123984341354,14.6106277774529,15.6088571207704,
16.6070864640879,17.6053158074054,18.6035451507229,19.6017744940404,20.600003837358,
21.5982331806755,22.596462523993,23.5946918673105,24.592921210628,25.5911505539455,
26.589379897263,27.5876092405805,28.585838583898,29.5840679272155,30.5822972705331,
31.5805266138506,32.5787559571681,33.5769853004856,34.5752146438031,35.5734439871206,
36.5716733304381,37.5699026737556,38.5681320170731,39.5663613603907,40.5645907037082,
41.5628200470257,42.5610493903432,43.5592787336607,44.5575080769782,45.5557374202957,
46.5539667636132,47.5521961069307,48.5504254502482,49.5486547935658,50.5468841368833,
51.5451134802008,52.5433428235183,53.5415721668358,54.5398015101533,55.5380308534708,
56.5362601967883,57.5344895401058,58.5327188834233,59.5309482267409,60.5291775700584,
61.5274069133759,62.5256362566934,63.5238656000109,64.5220949433284,65.5203242866459,
66.5185536299634,67.5167829732809,68.5150123165984,69.513241659916,70.5114710032335,
71.509700346551,72.5079296898685,73.506159033186,74.5043883765035,75.502617719821,
76.5008470631385,77.499076406456,78.4973057497735),.UNSPECIFIED.);
#253=B_SPLINE_SURFACE_WITH_KNOTS('',3,3,((#40037,#40038,#40039,#40040,#40041,
#40042,#40043,#40044,#40045,#40046,#40047,#40048,#40049,#40050,#40051,#40052,
#40053,#40054,#40055,#40056,#40057,#40058,#40059,#40060,#40061,#40062,#40063,
#40064,#40065,#40066,#40067,#40068,#40069,#40070,#40071,#40072,#40073,#40074,
#40075,#40076,#40077,#40078,#40079,#40080,#40081,#40082,#40083,#40084,#40085,
#40086,#40087,#40088,#40089,#40090,#40091,#40092,#40093,#40094,#40095,#40096,
#40097,#40098,#40099,#40100,#40101,#40102,#40103,#40104,#40105,#40106,#40107,
#40108),(#40109,#40110,#40111,#40112,#40113,#40114,#40115,#40116,#40117,
#40118,#40119,#40120,#40121,#40122,#40123,#40124,#40125,#40126,#40127,#40128,
#40129,#40130,#40131,#40132,#40133,#40134,#40135,#40136,#40137,#40138,#40139,
#40140,#40141,#40142,#40143,#40144,#40145,#40146,#40147,#40148,#40149,#40150,
#40151,#40152,#40153,#40154,#40155,#40156,#40157,#40158,#40159,#40160,#40161,
#40162,#40163,#40164,#40165,#40166,#40167,#40168,#40169,#40170,#40171,#40172,
#40173,#40174,#40175,#40176,#40177,#40178,#40179,#40180),(#40181,#40182,
#40183,#40184,#40185,#40186,#40187,#40188,#40189,#40190,#40191,#40192,#40193,
#40194,#40195,#40196,#40197,#40198,#40199,#40200,#40201,#40202,#40203,#40204,
#40205,#40206,#40207,#40208,#40209,#40210,#40211,#40212,#40213,#40214,#40215,
#40216,#40217,#40218,#40219,#40220,#40221,#40222,#40223,#40224,#40225,#40226,
#40227,#40228,#40229,#40230,#40231,#40232,#40233,#40234,#40235,#40236,#40237,
#40238,#40239,#40240,#40241,#40242,#40243,#40244,#40245,#40246,#40247,#40248,
#40249,#40250,#40251,#40252),(#40253,#40254,#40255,#40256,#40257,#40258,
#40259,#40260,#40261,#40262,#40263,#40264,#40265,#40266,#40267,#40268,#40269,
#40270,#40271,#40272,#40273,#40274,#40275,#40276,#40277,#40278,#40279,#40280,
#40281,#40282,#40283,#40284,#40285,#40286,#40287,#40288,#40289,#40290,#40291,
#40292,#40293,#40294,#40295,#40296,#40297,#40298,#40299,#40300,#40301,#40302,
#40303,#40304,#40305,#40306,#40307,#40308,#40309,#40310,#40311,#40312,#40313,
#40314,#40315,#40316,#40317,#40318,#40319,#40320,#40321,#40322,#40323,#40324)),
 .UNSPECIFIED.,.F.,.F.,.F.,(4,4),(4,1,1,1,1,1,1,1,1,1,1,1,1,1,1,1,1,1,1,
1,1,1,1,1,1,1,1,1,1,1,1,1,1,1,1,1,1,1,1,1,1,1,1,1,1,1,1,1,1,1,1,1,1,1,1,
1,1,1,1,1,1,1,1,1,1,1,1,1,1,4),(0.,0.0329955678841871),(8.30203615430834,
9.30137729453432,10.3007184347603,11.3000595749863,12.2994007152123,13.2987418554383,
14.2980829956642,15.2974241358902,16.2967652761162,17.2961064163422,18.2954475565682,
19.2947886967942,20.2941298370201,21.2934709772461,22.2928121174721,23.2921532576981,
24.2914943979241,25.2908355381501,26.290176678376,27.289517818602,28.288858958828,
29.288200099054,30.28754123928,31.286882379506,32.2862235197319,33.2855646599579,
34.2849058001839,35.2842469404099,36.2835880806359,37.2829292208619,38.2822703610879,
39.2816115013138,40.2809526415398,41.2802937817658,42.2796349219918,43.2789760622178,
44.2783172024438,45.2776583426697,46.2769994828957,47.2763406231217,48.2756817633477,
49.2750229035737,50.2743640437997,51.2737051840256,52.2730463242516,53.2723874644776,
54.2717286047036,55.2710697449296,56.2704108851556,57.2697520253815,58.2690931656075,
59.2684343058335,60.2677754460595,61.2671165862855,62.2664577265115,63.2657988667374,
64.2651400069634,65.2644811471894,66.2638222874154,67.2631634276414,68.2625045678674,
69.2618457080933,70.2611868483193,71.2605279885453,72.2598691287713,73.2592102689973,
74.2585514092233,75.2578925494492,76.2572336896752,77.2565748299012),
 .UNSPECIFIED.);
#325=FACE_BOUND('',#1720,.T.);
#326=FACE_BOUND('',#1723,.T.);
#454=PLANE('',#12136);
#455=PLANE('',#12137);
#456=PLANE('',#12138);
#457=PLANE('',#12139);
#458=PLANE('',#12140);
#459=PLANE('',#12141);
#460=PLANE('',#12142);
#461=PLANE('',#12143);
#462=PLANE('',#12147);
#463=PLANE('',#12148);
#998=FACE_OUTER_BOUND('',#1687,.T.);
#999=FACE_OUTER_BOUND('',#1688,.T.);
#1000=FACE_OUTER_BOUND('',#1689,.T.);
#1001=FACE_OUTER_BOUND('',#1690,.T.);
#1002=FACE_OUTER_BOUND('',#1691,.T.);
#1003=FACE_OUTER_BOUND('',#1692,.T.);
#1004=FACE_OUTER_BOUND('',#1693,.T.);
#1005=FACE_OUTER_BOUND('',#1694,.T.);
#1006=FACE_OUTER_BOUND('',#1695,.T.);
#1007=FACE_OUTER_BOUND('',#1696,.T.);
#1008=FACE_OUTER_BOUND('',#1697,.T.);
#1009=FACE_OUTER_BOUND('',#1698,.T.);
#1010=FACE_OUTER_BOUND('',#1699,.T.);
#1011=FACE_OUTER_BOUND('',#1700,.T.);
#1012=FACE_OUTER_BOUND('',#1701,.T.);
#1013=FACE_OUTER_BOUND('',#1702,.T.);
#1014=FACE_OUTER_BOUND('',#1703,.T.);
#1015=FACE_OUTER_BOUND('',#1704,.T.);
#1016=FACE_OUTER_BOUND('',#1705,.T.);
#1017=FACE_OUTER_BOUND('',#1706,.T.);
#1018=FACE_OUTER_BOUND('',#1707,.T.);
#1019=FACE_OUTER_BOUND('',#1708,.T.);
#1020=FACE_OUTER_BOUND('',#1709,.T.);
#1021=FACE_OUTER_BOUND('',#1710,.T.);
#1022=FACE_OUTER_BOUND('',#1711,.T.);
#1023=FACE_OUTER_BOUND('',#1712,.T.);
#1024=FACE_OUTER_BOUND('',#1713,.T.);
#1025=FACE_OUTER_BOUND('',#1714,.T.);
#1026=FACE_OUTER_BOUND('',#1715,.T.);
#1027=FACE_OUTER_BOUND('',#1716,.T.);
#1028=FACE_OUTER_BOUND('',#1717,.T.);
#1029=FACE_OUTER_BOUND('',#1718,.T.);
#1030=FACE_OUTER_BOUND('',#1719,.T.);
#1031=FACE_OUTER_BOUND('',#1721,.T.);
#1032=FACE_OUTER_BOUND('',#1722,.T.);
#1033=FACE_OUTER_BOUND('',#1724,.T.);
#1687=EDGE_LOOP('',(#9607,#9608,#9609,#9610));
#1688=EDGE_LOOP('',(#9611,#9612,#9613,#9614));
#1689=EDGE_LOOP('',(#9615,#9616,#9617,#9618));
#1690=EDGE_LOOP('',(#9619,#9620,#9621,#9622));
#1691=EDGE_LOOP('',(#9623,#9624,#9625,#9626));
#1692=EDGE_LOOP('',(#9627,#9628,#9629,#9630));
#1693=EDGE_LOOP('',(#9631,#9632,#9633,#9634));
#1694=EDGE_LOOP('',(#9635,#9636,#9637,#9638));
#1695=EDGE_LOOP('',(#9639,#9640,#9641,#9642));
#1696=EDGE_LOOP('',(#9643,#9644,#9645,#9646));
#1697=EDGE_LOOP('',(#9647,#9648,#9649,#9650));
#1698=EDGE_LOOP('',(#9651,#9652,#9653,#9654));
#1699=EDGE_LOOP('',(#9655,#9656,#9657,#9658));
#1700=EDGE_LOOP('',(#9659,#9660,#9661,#9662));
#1701=EDGE_LOOP('',(#9663,#9664,#9665,#9666));
#1702=EDGE_LOOP('',(#9667,#9668,#9669,#9670));
#1703=EDGE_LOOP('',(#9671,#9672,#9673,#9674));
#1704=EDGE_LOOP('',(#9675,#9676,#9677,#9678));
#1705=EDGE_LOOP('',(#9679,#9680,#9681,#9682));
#1706=EDGE_LOOP('',(#9683,#9684,#9685,#9686));
#1707=EDGE_LOOP('',(#9687,#9688,#9689,#9690,#9691,#9692,#9693,#9694));
#1708=EDGE_LOOP('',(#9695,#9696,#9697,#9698,#9699,#9700,#9701,#9702,#9703,
#9704,#9705,#9706,#9707,#9708,#9709,#9710,#9711,#9712,#9713,#9714,#9715,
#9716,#9717,#9718));
#1709=EDGE_LOOP('',(#9719,#9720,#9721,#9722));
#1710=EDGE_LOOP('',(#9723,#9724,#9725,#9726,#9727,#9728,#9729,#9730,#9731,
#9732,#9733,#9734,#9735,#9736,#9737,#9738,#9739,#9740,#9741,#9742,#9743,
#9744,#9745,#9746,#9747));
#1711=EDGE_LOOP('',(#9748,#9749,#9750,#9751));
#1712=EDGE_LOOP('',(#9752,#9753,#9754,#9755));
#1713=EDGE_LOOP('',(#9756,#9757,#9758,#9759));
#1714=EDGE_LOOP('',(#9760,#9761,#9762,#9763));
#1715=EDGE_LOOP('',(#9764,#9765,#9766,#9767));
#1716=EDGE_LOOP('',(#9768,#9769,#9770,#9771));
#1717=EDGE_LOOP('',(#9772,#9773,#9774,#9775));
#1718=EDGE_LOOP('',(#9776,#9777,#9778,#9779,#9780,#9781));
#1719=EDGE_LOOP('',(#9782));
#1720=EDGE_LOOP('',(#9783,#9784,#9785,#9786));
#1721=EDGE_LOOP('',(#9787,#9788,#9789,#9790));
#1722=EDGE_LOOP('',(#9791));
#1723=EDGE_LOOP('',(#9792,#9793,#9794,#9795,#9796,#9797));
#1724=EDGE_LOOP('',(#9798));
#1971=CIRCLE('',#12109,0.14635);
#1972=CIRCLE('',#12120,0.117775);
#1973=CIRCLE('',#12131,0.14635);
#1974=CIRCLE('',#12132,0.05);
#1975=CIRCLE('',#12134,0.117775);
#1976=CIRCLE('',#12144,0.3);
#1977=CIRCLE('',#12146,0.3);
#2683=B_SPLINE_CURVE_WITH_KNOTS('',3,(#38774,#38775,#38776,#38777,#38778,
#38779,#38780,#38781,#38782,#38783),.UNSPECIFIED.,.F.,.F.,(4,3,3,4),(-4.09202352044854,
-3.99291737327004,-2.99468802995253,-2.07317267331973),.UNSPECIFIED.);
#2684=B_SPLINE_CURVE_WITH_KNOTS('',3,(#38786,#38787,#38788,#38789,#38790,
#38791,#38792),.UNSPECIFIED.,.F.,.F.,(4,3,4),(0.,0.999341140225982,1.12274180646093),
 .UNSPECIFIED.);
#2685=B_SPLINE_CURVE_WITH_KNOTS('',3,(#38797,#38798,#38799,#38800,#38801,
#38802,#38803,#38804,#38805,#38806,#38807,#38808,#38809,#38810,#38811,#38812,
#38813,#38814,#38815,#38816,#38817,#38818),.UNSPECIFIED.,.F.,.F.,(4,3,3,
3,3,3,3,4),(-10.3752088276281,-9.9822934331751,-8.98406408985759,-7.98583474654008,
-6.98760540322257,-5.98937605990506,-4.99114671658755,-4.09202352044854),
 .UNSPECIFIED.);
#2686=B_SPLINE_CURVE_WITH_KNOTS('',3,(#38819,#38820,#38821,#38822,#38823,
#38824,#38825,#38826,#38827,#38828,#38829,#38830,#38831,#38832,#38833,#38834,
#38835,#38836,#38837,#38838,#38839,#38840),.UNSPECIFIED.,.F.,.F.,(4,3,3,
3,3,3,3,4),(1.12274180646093,1.99868228045197,2.99802342067795,3.99736456090394,
4.99670570112992,5.99604684135591,6.99538798158189,7.40592711364052),
 .UNSPECIFIED.);
#2687=B_SPLINE_CURVE_WITH_KNOTS('',3,(#38845,#38846,#38847,#38848,#38849,
#38850,#38851,#38852,#38853,#38854,#38855,#38856,#38857,#38858,#38859,#38860,
#38861,#38862,#38863,#38864,#38865,#38866),.UNSPECIFIED.,.F.,.F.,(4,3,3,
3,3,3,3,4),(-16.6583941348077,-15.9716694930802,-14.9734401497627,-13.9752108064451,
-12.9769814631276,-11.9787521198101,-10.9805227764926,-10.3752088276281),
 .UNSPECIFIED.);
#2688=B_SPLINE_CURVE_WITH_KNOTS('',3,(#38867,#38868,#38869,#38870,#38871,
#38872,#38873,#38874,#38875,#38876,#38877,#38878,#38879,#38880,#38881,#38882,
#38883,#38884,#38885,#38886,#38887,#38888),.UNSPECIFIED.,.F.,.F.,(4,3,3,
3,3,3,3,4),(7.40592711364052,7.99472912180787,8.99407026203386,9.99341140225984,
10.9927525424858,11.9920936827118,12.9914348229378,13.6891124208201),
 .UNSPECIFIED.);
#2689=B_SPLINE_CURVE_WITH_KNOTS('',3,(#38893,#38894,#38895,#38896,#38897,
#38898,#38899,#38900,#38901,#38902,#38903,#38904,#38905,#38906,#38907,#38908,
#38909,#38910,#38911,#38912,#38913,#38914),.UNSPECIFIED.,.F.,.F.,(4,3,3,
3,3,3,3,4),(-22.9415794419873,-21.9610455529852,-20.9628162096677,-19.9645868663502,
-18.9663575230327,-17.9681281797152,-16.9698988363977,-16.6583941348077),
 .UNSPECIFIED.);
#2690=B_SPLINE_CURVE_WITH_KNOTS('',3,(#38915,#38916,#38917,#38918,#38919,
#38920,#38921,#38922,#38923,#38924,#38925,#38926,#38927,#38928,#38929,#38930,
#38931,#38932,#38933,#38934,#38935,#38936),.UNSPECIFIED.,.F.,.F.,(4,3,3,
3,3,3,3,4),(13.6891124208201,13.9907759631638,14.9901171033898,15.9894582436157,
16.9887993838417,17.9881405240677,18.9874816642937,19.9722977279997),
 .UNSPECIFIED.);
#2691=B_SPLINE_CURVE_WITH_KNOTS('',3,(#38941,#38942,#38943,#38944,#38945,
#38946,#38947,#38948,#38949,#38950,#38951,#38952,#38953,#38954,#38955,#38956,
#38957,#38958,#38959,#38960,#38961,#38962,#38963,#38964,#38965),
 .UNSPECIFIED.,.F.,.F.,(4,3,3,3,3,3,3,3,4),(-29.2247647491669,-28.9486509562078,
-27.9504216128903,-26.9521922695728,-25.9539629262553,-24.9557335829378,
-23.9575042396202,-22.9592748963027,-22.9415794419873),.UNSPECIFIED.);
#2692=B_SPLINE_CURVE_WITH_KNOTS('',3,(#38966,#38967,#38968,#38969,#38970,
#38971,#38972,#38973,#38974,#38975,#38976,#38977,#38978,#38979,#38980,#38981,
#38982,#38983,#38984,#38985,#38986,#38987,#38988,#38989,#38990),
 .UNSPECIFIED.,.F.,.F.,(4,3,3,3,3,3,3,3,4),(19.9722977279997,19.9868228045197,
20.9861639447457,21.9855050849716,22.9848462251976,23.9841873654236,24.9835285056496,
25.9828696458756,26.2554830351793),.UNSPECIFIED.);
#2693=B_SPLINE_CURVE_WITH_KNOTS('',3,(#38995,#38996,#38997,#38998,#38999,
#39000,#39001,#39002,#39003,#39004,#39005,#39006,#39007,#39008,#39009,#39010,
#39011,#39012,#39013,#39014,#39015,#39016),.UNSPECIFIED.,.F.,.F.,(4,3,3,
3,3,3,3,4),(-35.5079500563465,-34.9380270161129,-33.9397976727954,-32.9415683294778,
-31.9433389861603,-30.9451096428428,-29.9468802995253,-29.2247647491669),
 .UNSPECIFIED.);
#2694=B_SPLINE_CURVE_WITH_KNOTS('',3,(#39017,#39018,#39019,#39020,#39021,
#39022,#39023,#39024,#39025,#39026,#39027,#39028,#39029,#39030,#39031,#39032,
#39033,#39034,#39035,#39036,#39037,#39038),.UNSPECIFIED.,.F.,.F.,(4,3,3,
3,3,3,3,4),(26.2554830351793,26.9822107861016,27.9815519263275,28.9808930665535,
29.9802342067795,30.9795753470055,31.9789164872315,32.5386683423589),
 .UNSPECIFIED.);
#2695=B_SPLINE_CURVE_WITH_KNOTS('',3,(#39043,#39044,#39045,#39046,#39047,
#39048,#39049,#39050,#39051,#39052,#39053,#39054,#39055,#39056,#39057,#39058,
#39059,#39060,#39061,#39062,#39063,#39064),.UNSPECIFIED.,.F.,.F.,(4,3,3,
3,3,3,3,4),(-41.7911353635261,-40.9274030760179,-39.9291737327004,-38.9309443893829,
-37.9327150460654,-36.9344857027479,-35.9362563594304,-35.5079500563465),
 .UNSPECIFIED.);
#2696=B_SPLINE_CURVE_WITH_KNOTS('',3,(#39065,#39066,#39067,#39068,#39069,
#39070,#39071,#39072,#39073,#39074,#39075,#39076,#39077,#39078,#39079,#39080,
#39081,#39082,#39083,#39084,#39085,#39086),.UNSPECIFIED.,.F.,.F.,(4,3,3,
3,3,3,3,4),(32.5386683423589,32.9782576274575,33.9775987676834,34.9769399079094,
35.9762810481354,36.9756221883614,37.9749633285874,38.8218536495385),
 .UNSPECIFIED.);
#2697=B_SPLINE_CURVE_WITH_KNOTS('',3,(#39091,#39092,#39093,#39094,#39095,
#39096,#39097,#39098,#39099,#39100,#39101,#39102,#39103,#39104,#39105,#39106,
#39107,#39108,#39109,#39110,#39111,#39112,#39113,#39114,#39115),
 .UNSPECIFIED.,.F.,.F.,(4,3,3,3,3,3,3,3,4),(-48.0743206707057,-47.9150084792405,
-46.916779135923,-45.9185497926055,-44.920320449288,-43.9220911059705,-42.9238617626529,
-41.9256324193354,-41.7911353635261),.UNSPECIFIED.);
#2698=B_SPLINE_CURVE_WITH_KNOTS('',3,(#39116,#39117,#39118,#39119,#39120,
#39121,#39122,#39123,#39124,#39125,#39126,#39127,#39128,#39129,#39130,#39131,
#39132,#39133,#39134,#39135,#39136,#39137,#39138,#39139,#39140),
 .UNSPECIFIED.,.F.,.F.,(4,3,3,3,3,3,3,3,4),(38.8218536495385,38.9743044688134,
39.9736456090394,40.9729867492653,41.9723278894913,42.9716690297173,43.9710101699433,
44.9703513101693,45.105038956718),.UNSPECIFIED.);
#2699=B_SPLINE_CURVE_WITH_KNOTS('',3,(#39145,#39146,#39147,#39148,#39149,
#39150,#39151,#39152,#39153,#39154,#39155,#39156,#39157,#39158,#39159,#39160,
#39161,#39162,#39163,#39164,#39165,#39166),.UNSPECIFIED.,.F.,.F.,(4,3,3,
3,3,3,3,4),(-54.3575059778853,-53.9043845391456,-52.906155195828,-51.9079258525105,
-50.909696509193,-49.9114671658755,-48.913237822558,-48.0743206707057),
 .UNSPECIFIED.);
#2700=B_SPLINE_CURVE_WITH_KNOTS('',3,(#39167,#39168,#39169,#39170,#39171,
#39172,#39173,#39174,#39175,#39176,#39177,#39178,#39179,#39180,#39181,#39182,
#39183,#39184,#39185,#39186,#39187,#39188),.UNSPECIFIED.,.F.,.F.,(4,3,3,
3,3,3,3,4),(45.105038956718,45.9696924503953,46.9690335906212,47.9683747308472,
48.9677158710732,49.9670570112992,50.9663981515252,51.3882242638976),
 .UNSPECIFIED.);
#2701=B_SPLINE_CURVE_WITH_KNOTS('',3,(#39193,#39194,#39195,#39196,#39197,
#39198,#39199,#39200,#39201,#39202,#39203,#39204,#39205,#39206,#39207,#39208,
#39209,#39210,#39211,#39212,#39213,#39214),.UNSPECIFIED.,.F.,.F.,(4,3,3,
3,3,3,3,4),(-60.6406912850648,-59.8937605990506,-58.8955312557331,-57.8973019124156,
-56.8990725690981,-55.9008432257806,-54.9026138824631,-54.3575059778853),
 .UNSPECIFIED.);
#2702=B_SPLINE_CURVE_WITH_KNOTS('',3,(#39215,#39216,#39217,#39218,#39219,
#39220,#39221,#39222,#39223,#39224,#39225,#39226,#39227,#39228,#39229,#39230,
#39231,#39232,#39233,#39234,#39235,#39236),.UNSPECIFIED.,.F.,.F.,(4,3,3,
3,3,3,3,4),(51.3882242638976,51.9657392917511,52.9650804319771,53.9644215722031,
54.9637627124291,55.9631038526551,56.9624449928811,57.6714095710772),
 .UNSPECIFIED.);
#2703=B_SPLINE_CURVE_WITH_KNOTS('',3,(#39242,#39243,#39244,#39245,#39246,
#39247,#39248,#39249,#39250,#39251),.UNSPECIFIED.,.F.,.F.,(4,1,1,1,1,1,
1,4),(72.2566310325653,72.5079296898685,73.506159033186,74.5043883765035,
75.502617719821,76.5008470631385,77.499076406456,78.4973057497735),
 .UNSPECIFIED.);
#2704=B_SPLINE_CURVE_WITH_KNOTS('',3,(#39254,#39255,#39256,#39257,#39258,
#39259,#39260,#39261,#39262),.UNSPECIFIED.,.F.,.F.,(4,1,1,1,1,1,4),(72.2566310325652,
72.2598691287713,73.2592102689973,74.2585514092233,75.2578925494492,76.2572336896752,
77.2565748299012),.UNSPECIFIED.);
#2705=B_SPLINE_CURVE_WITH_KNOTS('',3,(#39267,#39268,#39269,#39270,#39271,
#39272,#39273,#39274,#39275,#39276),.UNSPECIFIED.,.F.,.F.,(4,1,1,1,1,1,
1,4),(65.9734457253856,66.5185536299634,67.5167829732809,68.5150123165984,
69.513241659916,70.5114710032335,71.509700346551,72.2566310325653),
 .UNSPECIFIED.);
#2706=B_SPLINE_CURVE_WITH_KNOTS('',3,(#39277,#39278,#39279,#39280,#39281,
#39282,#39283,#39284,#39285,#39286),.UNSPECIFIED.,.F.,.F.,(4,1,1,1,1,1,
1,4),(65.9734457253856,66.2638222874154,67.2631634276414,68.2625045678674,
69.2618457080933,70.2611868483193,71.2605279885453,72.2566310325652),
 .UNSPECIFIED.);
#2707=B_SPLINE_CURVE_WITH_KNOTS('',3,(#39291,#39292,#39293,#39294,#39295,
#39296,#39297,#39298,#39299,#39300),.UNSPECIFIED.,.F.,.F.,(4,1,1,1,1,1,
1,4),(59.6902604182061,60.5291775700584,61.5274069133759,62.5256362566934,
63.5238656000109,64.5220949433284,65.5203242866459,65.9734457253856),
 .UNSPECIFIED.);
#2708=B_SPLINE_CURVE_WITH_KNOTS('',3,(#39301,#39302,#39303,#39304,#39305,
#39306,#39307,#39308,#39309,#39310),.UNSPECIFIED.,.F.,.F.,(4,1,1,1,1,1,
1,4),(59.6902604182061,60.2677754460595,61.2671165862855,62.2664577265115,
63.2657988667374,64.2651400069634,65.2644811471894,65.9734457253856),
 .UNSPECIFIED.);
#2709=B_SPLINE_CURVE_WITH_KNOTS('',3,(#39315,#39316,#39317,#39318,#39319,
#39320,#39321,#39322,#39323,#39324,#39325),.UNSPECIFIED.,.F.,.F.,(4,1,1,
1,1,1,1,1,4),(53.4070751110265,53.5415721668358,54.5398015101533,55.5380308534708,
56.5362601967883,57.5344895401058,58.5327188834233,59.5309482267409,59.6902604182061),
 .UNSPECIFIED.);
#2710=B_SPLINE_CURVE_WITH_KNOTS('',3,(#39326,#39327,#39328,#39329,#39330,
#39331,#39332,#39333,#39334,#39335),.UNSPECIFIED.,.F.,.F.,(4,1,1,1,1,1,
1,4),(53.4070751110265,54.2717286047036,55.2710697449296,56.2704108851556,
57.2697520253815,58.2690931656075,59.2684343058335,59.6902604182061),
 .UNSPECIFIED.);
#2711=B_SPLINE_CURVE_WITH_KNOTS('',3,(#39340,#39341,#39342,#39343,#39344,
#39345,#39346,#39347,#39348,#39349),.UNSPECIFIED.,.F.,.F.,(4,1,1,1,1,1,
1,4),(47.1238898038469,47.5521961069307,48.5504254502482,49.5486547935658,
50.5468841368833,51.5451134802008,52.5433428235183,53.4070751110265),
 .UNSPECIFIED.);
#2712=B_SPLINE_CURVE_WITH_KNOTS('',3,(#39350,#39351,#39352,#39353,#39354,
#39355,#39356,#39357,#39358,#39359,#39360),.UNSPECIFIED.,.F.,.F.,(4,1,1,
1,1,1,1,1,4),(47.1238898038469,47.2763406231217,48.2756817633477,49.2750229035737,
50.2743640437997,51.2737051840256,52.2730463242516,53.2723874644776,53.4070751110265),
 .UNSPECIFIED.);
#2713=B_SPLINE_CURVE_WITH_KNOTS('',3,(#39365,#39366,#39367,#39368,#39369,
#39370,#39371,#39372,#39373,#39374),.UNSPECIFIED.,.F.,.F.,(4,1,1,1,1,1,
1,4),(40.8407044966673,41.5628200470257,42.5610493903432,43.5592787336607,
44.5575080769782,45.5557374202957,46.5539667636132,47.1238898038469),
 .UNSPECIFIED.);
#2714=B_SPLINE_CURVE_WITH_KNOTS('',3,(#39375,#39376,#39377,#39378,#39379,
#39380,#39381,#39382,#39383,#39384),.UNSPECIFIED.,.F.,.F.,(4,1,1,1,1,1,
1,4),(40.8407044966673,41.2802937817658,42.2796349219918,43.2789760622178,
44.2783172024438,45.2776583426697,46.2769994828957,47.1238898038469),
 .UNSPECIFIED.);
#2715=B_SPLINE_CURVE_WITH_KNOTS('',3,(#39389,#39390,#39391,#39392,#39393,
#39394,#39395,#39396,#39397,#39398,#39399),.UNSPECIFIED.,.F.,.F.,(4,1,1,
1,1,1,1,1,4),(34.5575191894877,34.5752146438031,35.5734439871206,36.5716733304381,
37.5699026737556,38.5681320170731,39.5663613603907,40.5645907037082,40.8407044966673),
 .UNSPECIFIED.);
#2716=B_SPLINE_CURVE_WITH_KNOTS('',3,(#39400,#39401,#39402,#39403,#39404,
#39405,#39406,#39407,#39408,#39409),.UNSPECIFIED.,.F.,.F.,(4,1,1,1,1,1,
1,4),(34.5575191894877,35.2842469404099,36.2835880806359,37.2829292208619,
38.2822703610879,39.2816115013138,40.2809526415398,40.8407044966673),
 .UNSPECIFIED.);
#2717=B_SPLINE_CURVE_WITH_KNOTS('',3,(#39414,#39415,#39416,#39417,#39418,
#39419,#39420,#39421,#39422,#39423),.UNSPECIFIED.,.F.,.F.,(4,1,1,1,1,1,
1,4),(28.2743338823081,28.585838583898,29.5840679272155,30.5822972705331,
31.5805266138506,32.5787559571681,33.5769853004856,34.5575191894877),
 .UNSPECIFIED.);
#2718=B_SPLINE_CURVE_WITH_KNOTS('',3,(#39424,#39425,#39426,#39427,#39428,
#39429,#39430,#39431,#39432,#39433,#39434),.UNSPECIFIED.,.F.,.F.,(4,1,1,
1,1,1,1,1,4),(28.2743338823081,28.288858958828,29.288200099054,30.28754123928,
31.286882379506,32.2862235197319,33.2855646599579,34.2849058001839,34.5575191894877),
 .UNSPECIFIED.);
#2719=B_SPLINE_CURVE_WITH_KNOTS('',3,(#39439,#39440,#39441,#39442,#39443,
#39444,#39445,#39446,#39447,#39448),.UNSPECIFIED.,.F.,.F.,(4,1,1,1,1,1,
1,4),(21.9911485751285,22.596462523993,23.5946918673105,24.592921210628,
25.5911505539455,26.589379897263,27.5876092405805,28.2743338823081),
 .UNSPECIFIED.);
#2720=B_SPLINE_CURVE_WITH_KNOTS('',3,(#39449,#39450,#39451,#39452,#39453,
#39454,#39455,#39456,#39457,#39458),.UNSPECIFIED.,.F.,.F.,(4,1,1,1,1,1,
1,4),(21.9911485751285,22.2928121174721,23.2921532576981,24.2914943979241,
25.2908355381501,26.290176678376,27.289517818602,28.2743338823081),
 .UNSPECIFIED.);
#2721=B_SPLINE_CURVE_WITH_KNOTS('',3,(#39463,#39464,#39465,#39466,#39467,
#39468,#39469,#39470,#39471,#39472),.UNSPECIFIED.,.F.,.F.,(4,1,1,1,1,1,
1,4),(15.7079632679489,16.6070864640879,17.6053158074054,18.6035451507229,
19.6017744940404,20.600003837358,21.5982331806755,21.9911485751285),
 .UNSPECIFIED.);
#2722=B_SPLINE_CURVE_WITH_KNOTS('',3,(#39473,#39474,#39475,#39476,#39477,
#39478,#39479,#39480,#39481,#39482),.UNSPECIFIED.,.F.,.F.,(4,1,1,1,1,1,
1,4),(15.7079632679489,16.2967652761162,17.2961064163422,18.2954475565682,
19.2947886967942,20.2941298370201,21.2934709772461,21.9911485751285),
 .UNSPECIFIED.);
#2723=B_SPLINE_CURVE_WITH_KNOTS('',3,(#39485,#39486,#39487,#39488,#39489,
#39490,#39491,#39492,#39493,#39494,#39495,#39496,#39497,#39498,#39499,#39500,
#39501,#39502,#39503,#39504,#39505,#39506,#39507,#39508,#39509,#39510,#39511,
#39512,#39513,#39514,#39515,#39516,#39517,#39518,#39519,#39520,#39521,#39522,
#39523,#39524,#39525,#39526,#39527,#39528,#39529,#39530,#39531,#39532,#39533,
#39534,#39535,#39536,#39537,#39538,#39539,#39540,#39541,#39542,#39543,#39544,
#39545,#39546,#39547,#39548,#39549,#39550,#39551,#39552,#39553,#39554,#39555,
#39556,#39557,#39558,#39559,#39560,#39561,#39562,#39563,#39564,#39565,#39566,
#39567,#39568,#39569,#39570,#39571,#39572,#39573,#39574,#39575,#39576,#39577,
#39578,#39579,#39580,#39581,#39582,#39583,#39584,#39585,#39586,#39587,#39588,
#39589,#39590,#39591,#39592,#39593,#39594,#39595,#39596,#39597,#39598,#39599,
#39600,#39601,#39602,#39603,#39604,#39605,#39606,#39607,#39608),
 .UNSPECIFIED.,.F.,.F.,(4,3,3,3,3,3,3,3,3,3,3,3,3,3,3,3,3,3,3,3,3,3,3,3,
3,3,3,3,3,3,3,3,3,3,3,3,3,3,3,3,3,4),(-0.753008129282183,-0.726412785409006,
-0.715916399573649,-0.694852053413067,-0.683242780289961,-0.673766450589417,
-0.652778815266657,-0.639500919906121,-0.631791179943898,-0.604637195598433,
-0.591408327349303,-0.58243092328052,-0.553935160168246,-0.540392555827386,
-0.528208940192808,-0.505508318677634,-0.491429191967348,-0.477982436820105,
-0.452062180399923,-0.438863938010204,-0.427153921531904,-0.400727666335641,
-0.382198730280871,-0.374301411139377,-0.345303428221882,-0.331998698266984,
-0.322788462765202,-0.292662279142726,-0.279737557595205,-0.270213961274558,
-0.2400599353808,-0.238094602813322,-0.224912522130576,-0.21640841250359,
-0.186556730675161,-0.170795284707343,-0.161336087437576,-0.129168886313724,
-0.116523493465494,-0.106577361616136,-0.097001685189873,-0.096536015547866),
 .UNSPECIFIED.);
#2724=B_SPLINE_CURVE_WITH_KNOTS('',3,(#39610,#39611,#39612,#39613,#39614,
#39615,#39616,#39617,#39618,#39619,#39620,#39621,#39622,#39623,#39624,#39625,
#39626,#39627,#39628,#39629,#39630,#39631,#39632,#39633,#39634,#39635,#39636,
#39637,#39638,#39639,#39640,#39641,#39642,#39643,#39644,#39645,#39646),
 .UNSPECIFIED.,.F.,.F.,(4,3,3,3,3,3,3,3,3,3,3,3,4),(-0.204609524178328,
-0.17392271218969,-0.152224313672341,-0.142809800777549,-0.129914959151416,
-0.113620867578377,-0.100585910230378,-0.0924114342381335,-0.0693085756786001,
-0.0545304238088379,-0.0417479715798885,-0.0152833907299223,0.),
 .UNSPECIFIED.);
#2725=B_SPLINE_CURVE_WITH_KNOTS('',3,(#39649,#39650,#39651,#39652,#39653,
#39654,#39655,#39656,#39657,#39658,#39659,#39660,#39661,#39662,#39663,#39664),
 .UNSPECIFIED.,.F.,.F.,(4,3,3,3,3,4),(-0.096536015547866,-0.0724020116608995,
-0.0590251911255789,-0.0503900123732228,-0.0186970194324831,0.),
 .UNSPECIFIED.);
#2726=B_SPLINE_CURVE_WITH_KNOTS('',3,(#39949,#39950,#39951,#39952,#39953,
#39954,#39955,#39956),.UNSPECIFIED.,.F.,.F.,(4,1,1,1,1,4),(11.6159397475004,
12.6141690908179,13.6123984341354,14.6106277774529,15.6088571207704,15.7079632679489),
 .UNSPECIFIED.);
#2727=B_SPLINE_CURVE_WITH_KNOTS('',3,(#39957,#39958,#39959,#39960,#39961,
#39962,#39963,#39964,#39965,#39966,#39967,#39968,#39969,#39970,#39971,#39972,
#39973,#39974,#39975,#39976,#39977,#39978,#39979,#39980,#39981,#39982,#39983,
#39984,#39985,#39986,#39987,#39988,#39989,#39990,#39991,#39992,#39993,#39994,
#39995,#39996,#39997,#39998,#39999,#40000,#40001,#40002,#40003,#40004,#40005),
 .UNSPECIFIED.,.F.,.F.,(4,3,3,3,3,3,3,3,3,3,3,3,3,3,3,3,4),(-0.275362278356883,
-0.264159546247523,-0.242523917618953,-0.228489201611509,-0.209076761803474,
-0.198077656999141,-0.168436231356347,-0.151777330299101,-0.139830254922987,
-0.12544363295055,-0.101855794992709,-0.0891849033129337,-0.0668886774847003,
-0.0515641266869526,-0.0405229119346731,-0.0142790183076863,0.),
 .UNSPECIFIED.);
#2728=B_SPLINE_CURVE_WITH_KNOTS('',3,(#40006,#40007,#40008,#40009,#40010,
#40011,#40012,#40013,#40014,#40015,#40016,#40017,#40018,#40019,#40020,#40021,
#40022,#40023,#40024),.UNSPECIFIED.,.F.,.F.,(4,3,3,3,3,3,4),(-65.3636982725397,
-64.8849073156381,-63.8866779723206,-62.8884486290032,-61.8902192856856,
-60.8919899423681,-60.6406912850648),.UNSPECIFIED.);
#2729=B_SPLINE_CURVE_WITH_KNOTS('',3,(#40027,#40028,#40029,#40030,#40031,
#40032,#40033,#40034,#40035),.UNSPECIFIED.,.F.,.F.,(4,1,1,1,1,1,4),(10.375208827628,
11.3000595749863,12.2994007152123,13.2987418554383,14.2980829956642,15.2974241358902,
15.7079632679489),.UNSPECIFIED.);
#2730=B_SPLINE_CURVE_WITH_KNOTS('',3,(#40325,#40326,#40327,#40328,#40329,
#40330,#40331,#40332,#40333,#40334,#40335,#40336,#40337,#40338,#40339,#40340,
#40341,#40342,#40343,#40344,#40345,#40346),.UNSPECIFIED.,.F.,.F.,(4,3,3,
3,3,3,3,4),(57.6714095710772,57.9617861331071,58.961127273333,59.960468413559,
60.959809553785,61.959150694011,62.958491834237,63.29052559922),
 .UNSPECIFIED.);
#2731=B_SPLINE_CURVE_WITH_KNOTS('',3,(#40347,#40348,#40349,#40350,#40351,
#40352,#40353,#40354,#40355,#40356,#40357,#40358,#40359,#40360,#40361,#40362,
#40363,#40364,#40365,#40366,#40367,#40368,#40369,#40370,#40371,#40372,#40373,
#40374,#40375,#40376,#40377,#40378,#40379,#40380,#40381,#40382,#40383,#40384,
#40385,#40386,#40387,#40388,#40389,#40390,#40391,#40392,#40393,#40394,#40395,
#40396,#40397,#40398),.UNSPECIFIED.,.F.,.F.,(4,3,3,3,3,3,3,3,3,3,3,3,3,
3,3,3,3,4),(-0.276631791712725,-0.267716618892456,-0.246046101828633,-0.235289362386452,
-0.214941892616146,-0.204749662554743,-0.176256346031651,-0.161806307413905,
-0.15286753466007,-0.140652476775023,-0.120886137603943,-0.110226811379351,
-0.100669960776508,-0.0755024705823808,-0.058604244392821,-0.0491682800449266,
-0.0181536719473738,0.),.UNSPECIFIED.);
#3342=LINE('',#38772,#3974);
#3343=LINE('',#38796,#3975);
#3344=LINE('',#38844,#3976);
#3345=LINE('',#38892,#3977);
#3346=LINE('',#38940,#3978);
#3347=LINE('',#38994,#3979);
#3348=LINE('',#39042,#3980);
#3349=LINE('',#39090,#3981);
#3350=LINE('',#39144,#3982);
#3351=LINE('',#39192,#3983);
#3352=LINE('',#39240,#3984);
#3353=LINE('',#39266,#3985);
#3354=LINE('',#39290,#3986);
#3355=LINE('',#39314,#3987);
#3356=LINE('',#39339,#3988);
#3357=LINE('',#39364,#3989);
#3358=LINE('',#39388,#3990);
#3359=LINE('',#39413,#3991);
#3360=LINE('',#39438,#3992);
#3361=LINE('',#39462,#3993);
#3362=LINE('',#39666,#3994);
#3363=LINE('',#40403,#3995);
#3364=LINE('',#40405,#3996);
#3365=LINE('',#40407,#3997);
#3366=LINE('',#40408,#3998);
#3367=LINE('',#40411,#3999);
#3368=LINE('',#40413,#4000);
#3369=LINE('',#40414,#4001);
#3370=LINE('',#40417,#4002);
#3371=LINE('',#40419,#4003);
#3372=LINE('',#40420,#4004);
#3373=LINE('',#40423,#4005);
#3374=LINE('',#40425,#4006);
#3375=LINE('',#40426,#4007);
#3376=LINE('',#40429,#4008);
#3377=LINE('',#40431,#4009);
#3378=LINE('',#40432,#4010);
#3379=LINE('',#40434,#4011);
#3380=LINE('',#40435,#4012);
#3381=LINE('',#40442,#4013);
#3974=VECTOR('',#14125,0.15);
#3975=VECTOR('',#14130,0.15);
#3976=VECTOR('',#14133,0.15);
#3977=VECTOR('',#14136,0.15);
#3978=VECTOR('',#14139,0.15);
#3979=VECTOR('',#14142,0.15);
#3980=VECTOR('',#14145,0.15);
#3981=VECTOR('',#14148,0.15);
#3982=VECTOR('',#14151,0.15);
#3983=VECTOR('',#14154,0.15);
#3984=VECTOR('',#14157,0.117775);
#3985=VECTOR('',#14162,0.117775);
#3986=VECTOR('',#14165,0.117775);
#3987=VECTOR('',#14168,0.117775);
#3988=VECTOR('',#14171,0.117775);
#3989=VECTOR('',#14174,0.117775);
#3990=VECTOR('',#14177,0.117775);
#3991=VECTOR('',#14180,0.117775);
#3992=VECTOR('',#14183,0.117775);
#3993=VECTOR('',#14186,0.117775);
#3994=VECTOR('',#14191,0.1);
#3995=VECTOR('',#14202,1.);
#3996=VECTOR('',#14203,1.);
#3997=VECTOR('',#14204,1.);
#3998=VECTOR('',#14205,1.);
#3999=VECTOR('',#14208,1.);
#4000=VECTOR('',#14209,1.);
#4001=VECTOR('',#14210,1.);
#4002=VECTOR('',#14213,1.);
#4003=VECTOR('',#14214,1.);
#4004=VECTOR('',#14215,1.);
#4005=VECTOR('',#14218,1.);
#4006=VECTOR('',#14219,1.);
#4007=VECTOR('',#14220,1.);
#4008=VECTOR('',#14223,1.);
#4009=VECTOR('',#14224,1.);
#4010=VECTOR('',#14225,1.);
#4011=VECTOR('',#14228,1.);
#4012=VECTOR('',#14229,1.);
#4013=VECTOR('',#14238,0.3);
#5008=VERTEX_POINT('',#38770);
#5009=VERTEX_POINT('',#38771);
#5010=VERTEX_POINT('',#38773);
#5011=VERTEX_POINT('',#38784);
#5012=VERTEX_POINT('',#38794);
#5013=VERTEX_POINT('',#38795);
#5014=VERTEX_POINT('',#38842);
#5015=VERTEX_POINT('',#38843);
#5016=VERTEX_POINT('',#38890);
#5017=VERTEX_POINT('',#38891);
#5018=VERTEX_POINT('',#38938);
#5019=VERTEX_POINT('',#38939);
#5020=VERTEX_POINT('',#38992);
#5021=VERTEX_POINT('',#38993);
#5022=VERTEX_POINT('',#39040);
#5023=VERTEX_POINT('',#39041);
#5024=VERTEX_POINT('',#39088);
#5025=VERTEX_POINT('',#39089);
#5026=VERTEX_POINT('',#39142);
#5027=VERTEX_POINT('',#39143);
#5028=VERTEX_POINT('',#39190);
#5029=VERTEX_POINT('',#39191);
#5030=VERTEX_POINT('',#39238);
#5031=VERTEX_POINT('',#39239);
#5032=VERTEX_POINT('',#39241);
#5033=VERTEX_POINT('',#39252);
#5034=VERTEX_POINT('',#39264);
#5035=VERTEX_POINT('',#39265);
#5036=VERTEX_POINT('',#39288);
#5037=VERTEX_POINT('',#39289);
#5038=VERTEX_POINT('',#39312);
#5039=VERTEX_POINT('',#39313);
#5040=VERTEX_POINT('',#39337);
#5041=VERTEX_POINT('',#39338);
#5042=VERTEX_POINT('',#39362);
#5043=VERTEX_POINT('',#39363);
#5044=VERTEX_POINT('',#39386);
#5045=VERTEX_POINT('',#39387);
#5046=VERTEX_POINT('',#39411);
#5047=VERTEX_POINT('',#39412);
#5048=VERTEX_POINT('',#39436);
#5049=VERTEX_POINT('',#39437);
#5050=VERTEX_POINT('',#39460);
#5051=VERTEX_POINT('',#39461);
#5052=VERTEX_POINT('',#39484);
#5053=VERTEX_POINT('',#39609);
#5054=VERTEX_POINT('',#39647);
#5055=VERTEX_POINT('',#39665);
#5056=VERTEX_POINT('',#39948);
#5057=VERTEX_POINT('',#40026);
#5058=VERTEX_POINT('',#40401);
#5059=VERTEX_POINT('',#40402);
#5060=VERTEX_POINT('',#40404);
#5061=VERTEX_POINT('',#40406);
#5062=VERTEX_POINT('',#40410);
#5063=VERTEX_POINT('',#40412);
#5064=VERTEX_POINT('',#40416);
#5065=VERTEX_POINT('',#40418);
#5066=VERTEX_POINT('',#40422);
#5067=VERTEX_POINT('',#40424);
#5068=VERTEX_POINT('',#40428);
#5069=VERTEX_POINT('',#40430);
#5070=VERTEX_POINT('',#40438);
#5071=VERTEX_POINT('',#40441);
#6573=EDGE_CURVE('',#5008,#5009,#3342,.T.);
#6574=EDGE_CURVE('',#5008,#5010,#2683,.T.);
#6575=EDGE_CURVE('',#5010,#5011,#1971,.F.);
#6576=EDGE_CURVE('',#5011,#5009,#2684,.T.);
#6577=EDGE_CURVE('',#5012,#5013,#3343,.T.);
#6578=EDGE_CURVE('',#5012,#5008,#2685,.T.);
#6579=EDGE_CURVE('',#5009,#5013,#2686,.T.);
#6580=EDGE_CURVE('',#5014,#5015,#3344,.T.);
#6581=EDGE_CURVE('',#5014,#5012,#2687,.T.);
#6582=EDGE_CURVE('',#5013,#5015,#2688,.T.);
#6583=EDGE_CURVE('',#5016,#5017,#3345,.T.);
#6584=EDGE_CURVE('',#5016,#5014,#2689,.T.);
#6585=EDGE_CURVE('',#5015,#5017,#2690,.T.);
#6586=EDGE_CURVE('',#5018,#5019,#3346,.T.);
#6587=EDGE_CURVE('',#5018,#5016,#2691,.T.);
#6588=EDGE_CURVE('',#5017,#5019,#2692,.T.);
#6589=EDGE_CURVE('',#5020,#5021,#3347,.T.);
#6590=EDGE_CURVE('',#5020,#5018,#2693,.T.);
#6591=EDGE_CURVE('',#5019,#5021,#2694,.T.);
#6592=EDGE_CURVE('',#5022,#5023,#3348,.T.);
#6593=EDGE_CURVE('',#5022,#5020,#2695,.T.);
#6594=EDGE_CURVE('',#5021,#5023,#2696,.T.);
#6595=EDGE_CURVE('',#5024,#5025,#3349,.T.);
#6596=EDGE_CURVE('',#5024,#5022,#2697,.T.);
#6597=EDGE_CURVE('',#5023,#5025,#2698,.T.);
#6598=EDGE_CURVE('',#5026,#5027,#3350,.T.);
#6599=EDGE_CURVE('',#5026,#5024,#2699,.T.);
#6600=EDGE_CURVE('',#5025,#5027,#2700,.T.);
#6601=EDGE_CURVE('',#5028,#5029,#3351,.T.);
#6602=EDGE_CURVE('',#5028,#5026,#2701,.T.);
#6603=EDGE_CURVE('',#5027,#5029,#2702,.T.);
#6604=EDGE_CURVE('',#5030,#5031,#3352,.T.);
#6605=EDGE_CURVE('',#5030,#5032,#2703,.T.);
#6606=EDGE_CURVE('',#5032,#5033,#1972,.T.);
#6607=EDGE_CURVE('',#5031,#5033,#2704,.T.);
#6608=EDGE_CURVE('',#5034,#5035,#3353,.T.);
#6609=EDGE_CURVE('',#5034,#5030,#2705,.T.);
#6610=EDGE_CURVE('',#5035,#5031,#2706,.T.);
#6611=EDGE_CURVE('',#5036,#5037,#3354,.T.);
#6612=EDGE_CURVE('',#5036,#5034,#2707,.T.);
#6613=EDGE_CURVE('',#5037,#5035,#2708,.T.);
#6614=EDGE_CURVE('',#5038,#5039,#3355,.T.);
#6615=EDGE_CURVE('',#5038,#5036,#2709,.T.);
#6616=EDGE_CURVE('',#5039,#5037,#2710,.T.);
#6617=EDGE_CURVE('',#5040,#5041,#3356,.T.);
#6618=EDGE_CURVE('',#5040,#5038,#2711,.T.);
#6619=EDGE_CURVE('',#5041,#5039,#2712,.T.);
#6620=EDGE_CURVE('',#5042,#5043,#3357,.T.);
#6621=EDGE_CURVE('',#5042,#5040,#2713,.T.);
#6622=EDGE_CURVE('',#5043,#5041,#2714,.T.);
#6623=EDGE_CURVE('',#5044,#5045,#3358,.T.);
#6624=EDGE_CURVE('',#5044,#5042,#2715,.T.);
#6625=EDGE_CURVE('',#5045,#5043,#2716,.T.);
#6626=EDGE_CURVE('',#5046,#5047,#3359,.T.);
#6627=EDGE_CURVE('',#5046,#5044,#2717,.T.);
#6628=EDGE_CURVE('',#5047,#5045,#2718,.T.);
#6629=EDGE_CURVE('',#5048,#5049,#3360,.T.);
#6630=EDGE_CURVE('',#5048,#5046,#2719,.T.);
#6631=EDGE_CURVE('',#5049,#5047,#2720,.T.);
#6632=EDGE_CURVE('',#5050,#5051,#3361,.T.);
#6633=EDGE_CURVE('',#5050,#5048,#2721,.T.);
#6634=EDGE_CURVE('',#5051,#5049,#2722,.T.);
#6635=EDGE_CURVE('',#5033,#5052,#2723,.T.);
#6636=EDGE_CURVE('',#5053,#5032,#2724,.T.);
#6637=EDGE_CURVE('',#5054,#5053,#1973,.T.);
#6638=EDGE_CURVE('',#5052,#5054,#2725,.T.);
#6639=EDGE_CURVE('',#5052,#5055,#3362,.T.);
#6640=EDGE_CURVE('',#5055,#5055,#1974,.T.);
#6641=EDGE_CURVE('',#5056,#5050,#2726,.T.);
#6642=EDGE_CURVE('',#5010,#5056,#2727,.T.);
#6643=EDGE_CURVE('',#5053,#5028,#2728,.T.);
#6644=EDGE_CURVE('',#5057,#5051,#2729,.T.);
#6645=EDGE_CURVE('',#5056,#5057,#1975,.T.);
#6646=EDGE_CURVE('',#5029,#5054,#2730,.T.);
#6647=EDGE_CURVE('',#5057,#5011,#2731,.T.);
#6648=EDGE_CURVE('',#5058,#5059,#3363,.T.);
#6649=EDGE_CURVE('',#5058,#5060,#3364,.T.);
#6650=EDGE_CURVE('',#5060,#5061,#3365,.T.);
#6651=EDGE_CURVE('',#5059,#5061,#3366,.T.);
#6652=EDGE_CURVE('',#5062,#5058,#3367,.T.);
#6653=EDGE_CURVE('',#5062,#5063,#3368,.T.);
#6654=EDGE_CURVE('',#5063,#5060,#3369,.T.);
#6655=EDGE_CURVE('',#5064,#5062,#3370,.T.);
#6656=EDGE_CURVE('',#5064,#5065,#3371,.T.);
#6657=EDGE_CURVE('',#5065,#5063,#3372,.T.);
#6658=EDGE_CURVE('',#5066,#5064,#3373,.T.);
#6659=EDGE_CURVE('',#5066,#5067,#3374,.T.);
#6660=EDGE_CURVE('',#5067,#5065,#3375,.T.);
#6661=EDGE_CURVE('',#5068,#5066,#3376,.T.);
#6662=EDGE_CURVE('',#5068,#5069,#3377,.T.);
#6663=EDGE_CURVE('',#5069,#5067,#3378,.T.);
#6664=EDGE_CURVE('',#5059,#5068,#3379,.T.);
#6665=EDGE_CURVE('',#5061,#5069,#3380,.T.);
#6666=EDGE_CURVE('',#5070,#5070,#1976,.T.);
#6667=EDGE_CURVE('',#5070,#5071,#3381,.T.);
#6668=EDGE_CURVE('',#5071,#5071,#1977,.T.);
#9607=ORIENTED_EDGE('',*,*,#6573,.F.);
#9608=ORIENTED_EDGE('',*,*,#6574,.T.);
#9609=ORIENTED_EDGE('',*,*,#6575,.T.);
#9610=ORIENTED_EDGE('',*,*,#6576,.T.);
#9611=ORIENTED_EDGE('',*,*,#6577,.F.);
#9612=ORIENTED_EDGE('',*,*,#6578,.T.);
#9613=ORIENTED_EDGE('',*,*,#6573,.T.);
#9614=ORIENTED_EDGE('',*,*,#6579,.T.);
#9615=ORIENTED_EDGE('',*,*,#6580,.F.);
#9616=ORIENTED_EDGE('',*,*,#6581,.T.);
#9617=ORIENTED_EDGE('',*,*,#6577,.T.);
#9618=ORIENTED_EDGE('',*,*,#6582,.T.);
#9619=ORIENTED_EDGE('',*,*,#6583,.F.);
#9620=ORIENTED_EDGE('',*,*,#6584,.T.);
#9621=ORIENTED_EDGE('',*,*,#6580,.T.);
#9622=ORIENTED_EDGE('',*,*,#6585,.T.);
#9623=ORIENTED_EDGE('',*,*,#6586,.F.);
#9624=ORIENTED_EDGE('',*,*,#6587,.T.);
#9625=ORIENTED_EDGE('',*,*,#6583,.T.);
#9626=ORIENTED_EDGE('',*,*,#6588,.T.);
#9627=ORIENTED_EDGE('',*,*,#6589,.F.);
#9628=ORIENTED_EDGE('',*,*,#6590,.T.);
#9629=ORIENTED_EDGE('',*,*,#6586,.T.);
#9630=ORIENTED_EDGE('',*,*,#6591,.T.);
#9631=ORIENTED_EDGE('',*,*,#6592,.F.);
#9632=ORIENTED_EDGE('',*,*,#6593,.T.);
#9633=ORIENTED_EDGE('',*,*,#6589,.T.);
#9634=ORIENTED_EDGE('',*,*,#6594,.T.);
#9635=ORIENTED_EDGE('',*,*,#6595,.F.);
#9636=ORIENTED_EDGE('',*,*,#6596,.T.);
#9637=ORIENTED_EDGE('',*,*,#6592,.T.);
#9638=ORIENTED_EDGE('',*,*,#6597,.T.);
#9639=ORIENTED_EDGE('',*,*,#6598,.F.);
#9640=ORIENTED_EDGE('',*,*,#6599,.T.);
#9641=ORIENTED_EDGE('',*,*,#6595,.T.);
#9642=ORIENTED_EDGE('',*,*,#6600,.T.);
#9643=ORIENTED_EDGE('',*,*,#6601,.F.);
#9644=ORIENTED_EDGE('',*,*,#6602,.T.);
#9645=ORIENTED_EDGE('',*,*,#6598,.T.);
#9646=ORIENTED_EDGE('',*,*,#6603,.T.);
#9647=ORIENTED_EDGE('',*,*,#6604,.F.);
#9648=ORIENTED_EDGE('',*,*,#6605,.T.);
#9649=ORIENTED_EDGE('',*,*,#6606,.T.);
#9650=ORIENTED_EDGE('',*,*,#6607,.F.);
#9651=ORIENTED_EDGE('',*,*,#6608,.F.);
#9652=ORIENTED_EDGE('',*,*,#6609,.T.);
#9653=ORIENTED_EDGE('',*,*,#6604,.T.);
#9654=ORIENTED_EDGE('',*,*,#6610,.F.);
#9655=ORIENTED_EDGE('',*,*,#6611,.F.);
#9656=ORIENTED_EDGE('',*,*,#6612,.T.);
#9657=ORIENTED_EDGE('',*,*,#6608,.T.);
#9658=ORIENTED_EDGE('',*,*,#6613,.F.);
#9659=ORIENTED_EDGE('',*,*,#6614,.F.);
#9660=ORIENTED_EDGE('',*,*,#6615,.T.);
#9661=ORIENTED_EDGE('',*,*,#6611,.T.);
#9662=ORIENTED_EDGE('',*,*,#6616,.F.);
#9663=ORIENTED_EDGE('',*,*,#6617,.F.);
#9664=ORIENTED_EDGE('',*,*,#6618,.T.);
#9665=ORIENTED_EDGE('',*,*,#6614,.T.);
#9666=ORIENTED_EDGE('',*,*,#6619,.F.);
#9667=ORIENTED_EDGE('',*,*,#6620,.F.);
#9668=ORIENTED_EDGE('',*,*,#6621,.T.);
#9669=ORIENTED_EDGE('',*,*,#6617,.T.);
#9670=ORIENTED_EDGE('',*,*,#6622,.F.);
#9671=ORIENTED_EDGE('',*,*,#6623,.F.);
#9672=ORIENTED_EDGE('',*,*,#6624,.T.);
#9673=ORIENTED_EDGE('',*,*,#6620,.T.);
#9674=ORIENTED_EDGE('',*,*,#6625,.F.);
#9675=ORIENTED_EDGE('',*,*,#6626,.F.);
#9676=ORIENTED_EDGE('',*,*,#6627,.T.);
#9677=ORIENTED_EDGE('',*,*,#6623,.T.);
#9678=ORIENTED_EDGE('',*,*,#6628,.F.);
#9679=ORIENTED_EDGE('',*,*,#6629,.F.);
#9680=ORIENTED_EDGE('',*,*,#6630,.T.);
#9681=ORIENTED_EDGE('',*,*,#6626,.T.);
#9682=ORIENTED_EDGE('',*,*,#6631,.F.);
#9683=ORIENTED_EDGE('',*,*,#6632,.F.);
#9684=ORIENTED_EDGE('',*,*,#6633,.T.);
#9685=ORIENTED_EDGE('',*,*,#6629,.T.);
#9686=ORIENTED_EDGE('',*,*,#6634,.F.);
#9687=ORIENTED_EDGE('',*,*,#6635,.F.);
#9688=ORIENTED_EDGE('',*,*,#6606,.F.);
#9689=ORIENTED_EDGE('',*,*,#6636,.F.);
#9690=ORIENTED_EDGE('',*,*,#6637,.F.);
#9691=ORIENTED_EDGE('',*,*,#6638,.F.);
#9692=ORIENTED_EDGE('',*,*,#6639,.T.);
#9693=ORIENTED_EDGE('',*,*,#6640,.F.);
#9694=ORIENTED_EDGE('',*,*,#6639,.F.);
#9695=ORIENTED_EDGE('',*,*,#6636,.T.);
#9696=ORIENTED_EDGE('',*,*,#6605,.F.);
#9697=ORIENTED_EDGE('',*,*,#6609,.F.);
#9698=ORIENTED_EDGE('',*,*,#6612,.F.);
#9699=ORIENTED_EDGE('',*,*,#6615,.F.);
#9700=ORIENTED_EDGE('',*,*,#6618,.F.);
#9701=ORIENTED_EDGE('',*,*,#6621,.F.);
#9702=ORIENTED_EDGE('',*,*,#6624,.F.);
#9703=ORIENTED_EDGE('',*,*,#6627,.F.);
#9704=ORIENTED_EDGE('',*,*,#6630,.F.);
#9705=ORIENTED_EDGE('',*,*,#6633,.F.);
#9706=ORIENTED_EDGE('',*,*,#6641,.F.);
#9707=ORIENTED_EDGE('',*,*,#6642,.F.);
#9708=ORIENTED_EDGE('',*,*,#6574,.F.);
#9709=ORIENTED_EDGE('',*,*,#6578,.F.);
#9710=ORIENTED_EDGE('',*,*,#6581,.F.);
#9711=ORIENTED_EDGE('',*,*,#6584,.F.);
#9712=ORIENTED_EDGE('',*,*,#6587,.F.);
#9713=ORIENTED_EDGE('',*,*,#6590,.F.);
#9714=ORIENTED_EDGE('',*,*,#6593,.F.);
#9715=ORIENTED_EDGE('',*,*,#6596,.F.);
#9716=ORIENTED_EDGE('',*,*,#6599,.F.);
#9717=ORIENTED_EDGE('',*,*,#6602,.F.);
#9718=ORIENTED_EDGE('',*,*,#6643,.F.);
#9719=ORIENTED_EDGE('',*,*,#6632,.T.);
#9720=ORIENTED_EDGE('',*,*,#6644,.F.);
#9721=ORIENTED_EDGE('',*,*,#6645,.F.);
#9722=ORIENTED_EDGE('',*,*,#6641,.T.);
#9723=ORIENTED_EDGE('',*,*,#6635,.T.);
#9724=ORIENTED_EDGE('',*,*,#6638,.T.);
#9725=ORIENTED_EDGE('',*,*,#6646,.F.);
#9726=ORIENTED_EDGE('',*,*,#6603,.F.);
#9727=ORIENTED_EDGE('',*,*,#6600,.F.);
#9728=ORIENTED_EDGE('',*,*,#6597,.F.);
#9729=ORIENTED_EDGE('',*,*,#6594,.F.);
#9730=ORIENTED_EDGE('',*,*,#6591,.F.);
#9731=ORIENTED_EDGE('',*,*,#6588,.F.);
#9732=ORIENTED_EDGE('',*,*,#6585,.F.);
#9733=ORIENTED_EDGE('',*,*,#6582,.F.);
#9734=ORIENTED_EDGE('',*,*,#6579,.F.);
#9735=ORIENTED_EDGE('',*,*,#6576,.F.);
#9736=ORIENTED_EDGE('',*,*,#6647,.F.);
#9737=ORIENTED_EDGE('',*,*,#6644,.T.);
#9738=ORIENTED_EDGE('',*,*,#6634,.T.);
#9739=ORIENTED_EDGE('',*,*,#6631,.T.);
#9740=ORIENTED_EDGE('',*,*,#6628,.T.);
#9741=ORIENTED_EDGE('',*,*,#6625,.T.);
#9742=ORIENTED_EDGE('',*,*,#6622,.T.);
#9743=ORIENTED_EDGE('',*,*,#6619,.T.);
#9744=ORIENTED_EDGE('',*,*,#6616,.T.);
#9745=ORIENTED_EDGE('',*,*,#6613,.T.);
#9746=ORIENTED_EDGE('',*,*,#6610,.T.);
#9747=ORIENTED_EDGE('',*,*,#6607,.T.);
#9748=ORIENTED_EDGE('',*,*,#6601,.T.);
#9749=ORIENTED_EDGE('',*,*,#6646,.T.);
#9750=ORIENTED_EDGE('',*,*,#6637,.T.);
#9751=ORIENTED_EDGE('',*,*,#6643,.T.);
#9752=ORIENTED_EDGE('',*,*,#6648,.F.);
#9753=ORIENTED_EDGE('',*,*,#6649,.T.);
#9754=ORIENTED_EDGE('',*,*,#6650,.T.);
#9755=ORIENTED_EDGE('',*,*,#6651,.F.);
#9756=ORIENTED_EDGE('',*,*,#6652,.F.);
#9757=ORIENTED_EDGE('',*,*,#6653,.T.);
#9758=ORIENTED_EDGE('',*,*,#6654,.T.);
#9759=ORIENTED_EDGE('',*,*,#6649,.F.);
#9760=ORIENTED_EDGE('',*,*,#6655,.F.);
#9761=ORIENTED_EDGE('',*,*,#6656,.T.);
#9762=ORIENTED_EDGE('',*,*,#6657,.T.);
#9763=ORIENTED_EDGE('',*,*,#6653,.F.);
#9764=ORIENTED_EDGE('',*,*,#6658,.F.);
#9765=ORIENTED_EDGE('',*,*,#6659,.T.);
#9766=ORIENTED_EDGE('',*,*,#6660,.T.);
#9767=ORIENTED_EDGE('',*,*,#6656,.F.);
#9768=ORIENTED_EDGE('',*,*,#6661,.F.);
#9769=ORIENTED_EDGE('',*,*,#6662,.T.);
#9770=ORIENTED_EDGE('',*,*,#6663,.T.);
#9771=ORIENTED_EDGE('',*,*,#6659,.F.);
#9772=ORIENTED_EDGE('',*,*,#6664,.F.);
#9773=ORIENTED_EDGE('',*,*,#6651,.T.);
#9774=ORIENTED_EDGE('',*,*,#6665,.T.);
#9775=ORIENTED_EDGE('',*,*,#6662,.F.);
#9776=ORIENTED_EDGE('',*,*,#6665,.F.);
#9777=ORIENTED_EDGE('',*,*,#6650,.F.);
#9778=ORIENTED_EDGE('',*,*,#6654,.F.);
#9779=ORIENTED_EDGE('',*,*,#6657,.F.);
#9780=ORIENTED_EDGE('',*,*,#6660,.F.);
#9781=ORIENTED_EDGE('',*,*,#6663,.F.);
#9782=ORIENTED_EDGE('',*,*,#6666,.T.);
#9783=ORIENTED_EDGE('',*,*,#6642,.T.);
#9784=ORIENTED_EDGE('',*,*,#6645,.T.);
#9785=ORIENTED_EDGE('',*,*,#6647,.T.);
#9786=ORIENTED_EDGE('',*,*,#6575,.F.);
#9787=ORIENTED_EDGE('',*,*,#6666,.F.);
#9788=ORIENTED_EDGE('',*,*,#6667,.T.);
#9789=ORIENTED_EDGE('',*,*,#6668,.T.);
#9790=ORIENTED_EDGE('',*,*,#6667,.F.);
#9791=ORIENTED_EDGE('',*,*,#6668,.F.);
#9792=ORIENTED_EDGE('',*,*,#6648,.T.);
#9793=ORIENTED_EDGE('',*,*,#6664,.T.);
#9794=ORIENTED_EDGE('',*,*,#6661,.T.);
#9795=ORIENTED_EDGE('',*,*,#6658,.T.);
#9796=ORIENTED_EDGE('',*,*,#6655,.T.);
#9797=ORIENTED_EDGE('',*,*,#6652,.T.);
#9798=ORIENTED_EDGE('',*,*,#6640,.T.);
#10540=CYLINDRICAL_SURFACE('',#12108,0.14635);
#10541=CYLINDRICAL_SURFACE('',#12110,0.14635);
#10542=CYLINDRICAL_SURFACE('',#12111,0.14635);
#10543=CYLINDRICAL_SURFACE('',#12112,0.14635);
#10544=CYLINDRICAL_SURFACE('',#12113,0.14635);
#10545=CYLINDRICAL_SURFACE('',#12114,0.14635);
#10546=CYLINDRICAL_SURFACE('',#12115,0.14635);
#10547=CYLINDRICAL_SURFACE('',#12116,0.14635);
#10548=CYLINDRICAL_SURFACE('',#12117,0.14635);
#10549=CYLINDRICAL_SURFACE('',#12118,0.14635);
#10550=CYLINDRICAL_SURFACE('',#12119,0.117775);
#10551=CYLINDRICAL_SURFACE('',#12121,0.117775);
#10552=CYLINDRICAL_SURFACE('',#12122,0.117775);
#10553=CYLINDRICAL_SURFACE('',#12123,0.117775);
#10554=CYLINDRICAL_SURFACE('',#12124,0.117775);
#10555=CYLINDRICAL_SURFACE('',#12125,0.117775);
#10556=CYLINDRICAL_SURFACE('',#12126,0.117775);
#10557=CYLINDRICAL_SURFACE('',#12127,0.117775);
#10558=CYLINDRICAL_SURFACE('',#12128,0.117775);
#10559=CYLINDRICAL_SURFACE('',#12129,0.117775);
#10560=CYLINDRICAL_SURFACE('',#12133,0.117775);
#10561=CYLINDRICAL_SURFACE('',#12135,0.14635);
#10562=CYLINDRICAL_SURFACE('',#12145,0.3);
#11123=ADVANCED_FACE('',(#998),#10540,.T.);
#11124=ADVANCED_FACE('',(#999),#10541,.T.);
#11125=ADVANCED_FACE('',(#1000),#10542,.T.);
#11126=ADVANCED_FACE('',(#1001),#10543,.T.);
#11127=ADVANCED_FACE('',(#1002),#10544,.T.);
#11128=ADVANCED_FACE('',(#1003),#10545,.T.);
#11129=ADVANCED_FACE('',(#1004),#10546,.T.);
#11130=ADVANCED_FACE('',(#1005),#10547,.T.);
#11131=ADVANCED_FACE('',(#1006),#10548,.T.);
#11132=ADVANCED_FACE('',(#1007),#10549,.T.);
#11133=ADVANCED_FACE('',(#1008),#10550,.T.);
#11134=ADVANCED_FACE('',(#1009),#10551,.T.);
#11135=ADVANCED_FACE('',(#1010),#10552,.T.);
#11136=ADVANCED_FACE('',(#1011),#10553,.T.);
#11137=ADVANCED_FACE('',(#1012),#10554,.T.);
#11138=ADVANCED_FACE('',(#1013),#10555,.T.);
#11139=ADVANCED_FACE('',(#1014),#10556,.T.);
#11140=ADVANCED_FACE('',(#1015),#10557,.T.);
#11141=ADVANCED_FACE('',(#1016),#10558,.T.);
#11142=ADVANCED_FACE('',(#1017),#10559,.T.);
#11143=ADVANCED_FACE('',(#1018),#148,.T.);
#11144=ADVANCED_FACE('',(#1019),#252,.F.);
#11145=ADVANCED_FACE('',(#1020),#10560,.T.);
#11146=ADVANCED_FACE('',(#1021),#253,.F.);
#11147=ADVANCED_FACE('',(#1022),#10561,.T.);
#11148=ADVANCED_FACE('',(#1023),#454,.F.);
#11149=ADVANCED_FACE('',(#1024),#455,.F.);
#11150=ADVANCED_FACE('',(#1025),#456,.F.);
#11151=ADVANCED_FACE('',(#1026),#457,.F.);
#11152=ADVANCED_FACE('',(#1027),#458,.F.);
#11153=ADVANCED_FACE('',(#1028),#459,.F.);
#11154=ADVANCED_FACE('',(#1029),#460,.F.);
#11155=ADVANCED_FACE('',(#1030,#325),#461,.T.);
#11156=ADVANCED_FACE('',(#1031),#10562,.T.);
#11157=ADVANCED_FACE('',(#1032,#326),#462,.F.);
#11158=ADVANCED_FACE('',(#1033),#463,.T.);
#11245=CLOSED_SHELL('',(#11123,#11124,#11125,#11126,#11127,#11128,#11129,
#11130,#11131,#11132,#11133,#11134,#11135,#11136,#11137,#11138,#11139,#11140,
#11141,#11142,#11143,#11144,#11145,#11146,#11147,#11148,#11149,#11150,#11151,
#11152,#11153,#11154,#11155,#11156,#11157,#11158));
#12107=AXIS2_PLACEMENT_3D('',#38768,#14121,#14122);
#12108=AXIS2_PLACEMENT_3D('',#38769,#14123,#14124);
#12109=AXIS2_PLACEMENT_3D('',#38785,#14126,#14127);
#12110=AXIS2_PLACEMENT_3D('',#38793,#14128,#14129);
#12111=AXIS2_PLACEMENT_3D('',#38841,#14131,#14132);
#12112=AXIS2_PLACEMENT_3D('',#38889,#14134,#14135);
#12113=AXIS2_PLACEMENT_3D('',#38937,#14137,#14138);
#12114=AXIS2_PLACEMENT_3D('',#38991,#14140,#14141);
#12115=AXIS2_PLACEMENT_3D('',#39039,#14143,#14144);
#12116=AXIS2_PLACEMENT_3D('',#39087,#14146,#14147);
#12117=AXIS2_PLACEMENT_3D('',#39141,#14149,#14150);
#12118=AXIS2_PLACEMENT_3D('',#39189,#14152,#14153);
#12119=AXIS2_PLACEMENT_3D('',#39237,#14155,#14156);
#12120=AXIS2_PLACEMENT_3D('',#39253,#14158,#14159);
#12121=AXIS2_PLACEMENT_3D('',#39263,#14160,#14161);
#12122=AXIS2_PLACEMENT_3D('',#39287,#14163,#14164);
#12123=AXIS2_PLACEMENT_3D('',#39311,#14166,#14167);
#12124=AXIS2_PLACEMENT_3D('',#39336,#14169,#14170);
#12125=AXIS2_PLACEMENT_3D('',#39361,#14172,#14173);
#12126=AXIS2_PLACEMENT_3D('',#39385,#14175,#14176);
#12127=AXIS2_PLACEMENT_3D('',#39410,#14178,#14179);
#12128=AXIS2_PLACEMENT_3D('',#39435,#14181,#14182);
#12129=AXIS2_PLACEMENT_3D('',#39459,#14184,#14185);
#12130=AXIS2_PLACEMENT_3D('',#39483,#14187,#14188);
#12131=AXIS2_PLACEMENT_3D('',#39648,#14189,#14190);
#12132=AXIS2_PLACEMENT_3D('',#39667,#14192,#14193);
#12133=AXIS2_PLACEMENT_3D('',#40025,#14194,#14195);
#12134=AXIS2_PLACEMENT_3D('',#40036,#14196,#14197);
#12135=AXIS2_PLACEMENT_3D('',#40399,#14198,#14199);
#12136=AXIS2_PLACEMENT_3D('',#40400,#14200,#14201);
#12137=AXIS2_PLACEMENT_3D('',#40409,#14206,#14207);
#12138=AXIS2_PLACEMENT_3D('',#40415,#14211,#14212);
#12139=AXIS2_PLACEMENT_3D('',#40421,#14216,#14217);
#12140=AXIS2_PLACEMENT_3D('',#40427,#14221,#14222);
#12141=AXIS2_PLACEMENT_3D('',#40433,#14226,#14227);
#12142=AXIS2_PLACEMENT_3D('',#40436,#14230,#14231);
#12143=AXIS2_PLACEMENT_3D('',#40437,#14232,#14233);
#12144=AXIS2_PLACEMENT_3D('',#40439,#14234,#14235);
#12145=AXIS2_PLACEMENT_3D('',#40440,#14236,#14237);
#12146=AXIS2_PLACEMENT_3D('',#40443,#14239,#14240);
#12147=AXIS2_PLACEMENT_3D('',#40444,#14241,#14242);
#12148=AXIS2_PLACEMENT_3D('',#40445,#14243,#14244);
#14121=DIRECTION('axis',(0.,0.,1.));
#14122=DIRECTION('refdir',(1.,0.,0.));
#14123=DIRECTION('center_axis',(0.,0.,1.));
#14124=DIRECTION('ref_axis',(1.,0.,0.));
#14125=DIRECTION('',(0.,0.,-1.));
#14126=DIRECTION('center_axis',(0.,0.,-1.));
#14127=DIRECTION('ref_axis',(1.,0.,0.));
#14128=DIRECTION('center_axis',(0.,0.,1.));
#14129=DIRECTION('ref_axis',(1.,0.,0.));
#14130=DIRECTION('',(0.,0.,-1.));
#14131=DIRECTION('center_axis',(0.,0.,1.));
#14132=DIRECTION('ref_axis',(1.,0.,0.));
#14133=DIRECTION('',(0.,0.,-1.));
#14134=DIRECTION('center_axis',(0.,0.,1.));
#14135=DIRECTION('ref_axis',(1.,0.,0.));
#14136=DIRECTION('',(0.,0.,-1.));
#14137=DIRECTION('center_axis',(0.,0.,1.));
#14138=DIRECTION('ref_axis',(1.,0.,0.));
#14139=DIRECTION('',(0.,0.,-1.));
#14140=DIRECTION('center_axis',(0.,0.,1.));
#14141=DIRECTION('ref_axis',(1.,0.,0.));
#14142=DIRECTION('',(0.,0.,-1.));
#14143=DIRECTION('center_axis',(0.,0.,1.));
#14144=DIRECTION('ref_axis',(1.,0.,0.));
#14145=DIRECTION('',(0.,0.,-1.));
#14146=DIRECTION('center_axis',(0.,0.,1.));
#14147=DIRECTION('ref_axis',(1.,0.,0.));
#14148=DIRECTION('',(0.,0.,-1.));
#14149=DIRECTION('center_axis',(0.,0.,1.));
#14150=DIRECTION('ref_axis',(1.,0.,0.));
#14151=DIRECTION('',(0.,0.,-1.));
#14152=DIRECTION('center_axis',(0.,0.,1.));
#14153=DIRECTION('ref_axis',(1.,0.,0.));
#14154=DIRECTION('',(0.,0.,-1.));
#14155=DIRECTION('center_axis',(0.,0.,1.));
#14156=DIRECTION('ref_axis',(1.,7.53540174823413E-14,0.));
#14157=DIRECTION('',(0.,0.,1.));
#14158=DIRECTION('center_axis',(0.,0.,-1.));
#14159=DIRECTION('ref_axis',(1.,7.53540174823413E-14,0.));
#14160=DIRECTION('center_axis',(0.,0.,1.));
#14161=DIRECTION('ref_axis',(1.,7.53540174823413E-14,0.));
#14162=DIRECTION('',(0.,0.,1.));
#14163=DIRECTION('center_axis',(0.,0.,1.));
#14164=DIRECTION('ref_axis',(1.,7.53540174823413E-14,0.));
#14165=DIRECTION('',(0.,0.,1.));
#14166=DIRECTION('center_axis',(0.,0.,1.));
#14167=DIRECTION('ref_axis',(1.,7.53540174823413E-14,0.));
#14168=DIRECTION('',(0.,0.,1.));
#14169=DIRECTION('center_axis',(0.,0.,1.));
#14170=DIRECTION('ref_axis',(1.,7.53540174823413E-14,0.));
#14171=DIRECTION('',(0.,0.,1.));
#14172=DIRECTION('center_axis',(0.,0.,1.));
#14173=DIRECTION('ref_axis',(1.,7.53540174823413E-14,0.));
#14174=DIRECTION('',(0.,0.,1.));
#14175=DIRECTION('center_axis',(0.,0.,1.));
#14176=DIRECTION('ref_axis',(1.,7.53540174823413E-14,0.));
#14177=DIRECTION('',(0.,0.,1.));
#14178=DIRECTION('center_axis',(0.,0.,1.));
#14179=DIRECTION('ref_axis',(1.,7.53540174823413E-14,0.));
#14180=DIRECTION('',(0.,0.,1.));
#14181=DIRECTION('center_axis',(0.,0.,1.));
#14182=DIRECTION('ref_axis',(1.,7.53540174823413E-14,0.));
#14183=DIRECTION('',(0.,0.,1.));
#14184=DIRECTION('center_axis',(0.,0.,1.));
#14185=DIRECTION('ref_axis',(1.,7.53540174823413E-14,0.));
#14186=DIRECTION('',(0.,0.,1.));
#14187=DIRECTION('center_axis',(0.,0.,-1.));
#14188=DIRECTION('ref_axis',(1.,0.,0.));
#14189=DIRECTION('center_axis',(0.,0.,-1.));
#14190=DIRECTION('ref_axis',(1.,0.,0.));
#14191=DIRECTION('',(0.707106781186548,8.65956056235493E-17,0.707106781186547));
#14192=DIRECTION('center_axis',(0.,0.,1.));
#14193=DIRECTION('ref_axis',(1.,0.,0.));
#14194=DIRECTION('center_axis',(0.,0.,1.));
#14195=DIRECTION('ref_axis',(1.,7.53540174823413E-14,0.));
#14196=DIRECTION('center_axis',(0.,0.,-1.));
#14197=DIRECTION('ref_axis',(1.,7.53540174823413E-14,0.));
#14198=DIRECTION('center_axis',(0.,0.,1.));
#14199=DIRECTION('ref_axis',(1.,0.,0.));
#14200=DIRECTION('center_axis',(-2.40370335797945E-16,-1.,0.));
#14201=DIRECTION('ref_axis',(1.,-2.40370335797945E-16,0.));
#14202=DIRECTION('',(1.,-2.40370335797945E-16,0.));
#14203=DIRECTION('',(0.,0.,1.));
#14204=DIRECTION('',(1.,-2.40370335797945E-16,0.));
#14205=DIRECTION('',(0.,0.,1.));
#14206=DIRECTION('center_axis',(-0.866025403784439,-0.5,0.));
#14207=DIRECTION('ref_axis',(0.5,-0.866025403784439,0.));
#14208=DIRECTION('',(0.5,-0.866025403784439,0.));
#14209=DIRECTION('',(0.,0.,1.));
#14210=DIRECTION('',(0.5,-0.866025403784439,0.));
#14211=DIRECTION('center_axis',(-0.866025403784439,0.5,0.));
#14212=DIRECTION('ref_axis',(-0.5,-0.866025403784439,0.));
#14213=DIRECTION('',(-0.5,-0.866025403784439,0.));
#14214=DIRECTION('',(0.,0.,1.));
#14215=DIRECTION('',(-0.5,-0.866025403784439,0.));
#14216=DIRECTION('center_axis',(1.20185167898973E-16,1.,0.));
#14217=DIRECTION('ref_axis',(-1.,1.20185167898973E-16,0.));
#14218=DIRECTION('',(-1.,1.20185167898973E-16,0.));
#14219=DIRECTION('',(0.,0.,1.));
#14220=DIRECTION('',(-1.,1.20185167898973E-16,0.));
#14221=DIRECTION('center_axis',(0.866025403784439,0.5,0.));
#14222=DIRECTION('ref_axis',(-0.5,0.866025403784439,0.));
#14223=DIRECTION('',(-0.5,0.866025403784439,0.));
#14224=DIRECTION('',(0.,0.,1.));
#14225=DIRECTION('',(-0.5,0.866025403784439,0.));
#14226=DIRECTION('center_axis',(0.866025403784439,-0.5,0.));
#14227=DIRECTION('ref_axis',(0.5,0.866025403784439,0.));
#14228=DIRECTION('',(0.5,0.866025403784439,0.));
#14229=DIRECTION('',(0.5,0.866025403784439,0.));
#14230=DIRECTION('center_axis',(0.,0.,1.));
#14231=DIRECTION('ref_axis',(1.,0.,0.));
#14232=DIRECTION('center_axis',(0.,0.,1.));
#14233=DIRECTION('ref_axis',(1.,0.,0.));
#14234=DIRECTION('center_axis',(0.,0.,1.));
#14235=DIRECTION('ref_axis',(1.,0.,0.));
#14236=DIRECTION('center_axis',(0.,0.,1.));
#14237=DIRECTION('ref_axis',(1.,0.,0.));
#14238=DIRECTION('',(0.,0.,-1.));
#14239=DIRECTION('center_axis',(0.,0.,1.));
#14240=DIRECTION('ref_axis',(1.,0.,0.));
#14241=DIRECTION('center_axis',(0.,0.,1.));
#14242=DIRECTION('ref_axis',(1.,0.,0.));
#14243=DIRECTION('center_axis',(0.,0.,1.));
#14244=DIRECTION('ref_axis',(1.,0.,0.));
#38768=CARTESIAN_POINT('',(0.,0.,0.));
#38769=CARTESIAN_POINT('Origin',(0.,0.,0.));
#38770=CARTESIAN_POINT('',(-0.146530139441781,9.2983754875535E-5,0.0160655045842905));
#38771=CARTESIAN_POINT('',(-0.146482381647069,0.000161727750000726,0.00893449541570906));
#38772=CARTESIAN_POINT('',(-0.14635,-1.79227059055215E-17,0.));
#38773=CARTESIAN_POINT('',(0.0634007094575212,0.131904027763685,0.));
#38774=CARTESIAN_POINT('Ctrl Pts',(-0.146530139441781,9.2983754875535E-5,
0.0160655045842905));
#38775=CARTESIAN_POINT('Ctrl Pts',(-0.146562770122328,0.00491041321584185,
0.015802617364053));
#38776=CARTESIAN_POINT('Ctrl Pts',(-0.146345876989778,0.00972466734833348,
0.0155397301438155));
#38777=CARTESIAN_POINT('Ctrl Pts',(-0.145869825450435,0.0145129075872385,
0.015276842923578));
#38778=CARTESIAN_POINT('Ctrl Pts',(-0.141074879536054,0.0627416203906926,
0.0126289573514387));
#38779=CARTESIAN_POINT('Ctrl Pts',(-0.109987863649871,0.10833117855941,
0.00998107177929941));
#38780=CARTESIAN_POINT('Ctrl Pts',(-0.0668435938445389,0.130448755664999,
0.00733318620716011));
#38781=CARTESIAN_POINT('Ctrl Pts',(-0.0270149638383408,0.150866595604039,
0.00488879080477341));
#38782=CARTESIAN_POINT('Ctrl Pts',(0.0230889279919825,0.151281476944728,
0.00244439540238672));
#38783=CARTESIAN_POINT('Ctrl Pts',(0.0635548502597316,0.132093933345895,
1.98375346423187E-17));
#38784=CARTESIAN_POINT('',(-0.0634007094575231,0.131904027763684,0.));
#38785=CARTESIAN_POINT('Origin',(0.,0.,0.));
#38786=CARTESIAN_POINT('Ctrl Pts',(-0.063400709457523,0.131904027763684,
7.63278329429795E-17));
#38787=CARTESIAN_POINT('Ctrl Pts',(-0.107339749959442,0.110784382003545,
0.00265083470503432));
#38788=CARTESIAN_POINT('Ctrl Pts',(-0.139511904869873,0.0661645412785542,
0.00530166941006857));
#38789=CARTESIAN_POINT('Ctrl Pts',(-0.145460797893518,0.0180856147189845,
0.00795250411510281));
#38790=CARTESIAN_POINT('Ctrl Pts',(-0.146195379242097,0.0121487315761866,
0.00827983454863823));
#38791=CARTESIAN_POINT('Ctrl Pts',(-0.146530113272026,0.00615910494930538,
0.00860716498217364));
#38792=CARTESIAN_POINT('Ctrl Pts',(-0.146482381647069,0.000161727750000726,
0.00893449541570906));
#38793=CARTESIAN_POINT('Origin',(0.,0.,0.));
#38794=CARTESIAN_POINT('',(-0.146153148300412,8.02585168747302E-5,0.0660655045842906));
#38795=CARTESIAN_POINT('',(-0.146138869890956,7.0051777900314E-5,0.058934495415709));
#38796=CARTESIAN_POINT('',(-0.14635,-1.79227059055215E-17,0.));
#38797=CARTESIAN_POINT('Ctrl Pts',(-0.146153148300412,8.02585168747302E-5,
0.0660655045842906));
#38798=CARTESIAN_POINT('Ctrl Pts',(-0.146248563607689,0.0193075654691076,
0.0650232641302222));
#38799=CARTESIAN_POINT('Ctrl Pts',(-0.142725320554989,0.0385012587497889,
0.0639810236761539));
#38800=CARTESIAN_POINT('Ctrl Pts',(-0.135419901199499,0.0561272788093185,
0.0629387832220855));
#38801=CARTESIAN_POINT('Ctrl Pts',(-0.116859966748363,0.100907429136131,
0.0602908976499462));
#38802=CARTESIAN_POINT('Ctrl Pts',(-0.0738879770866151,0.13556903337647,
0.0576430120778069));
#38803=CARTESIAN_POINT('Ctrl Pts',(-0.0261938646990992,0.144231038496032,
0.0549951265056676));
#38804=CARTESIAN_POINT('Ctrl Pts',(0.0215002476884163,0.152893043615593,
0.0523472409335283));
#38805=CARTESIAN_POINT('Ctrl Pts',(0.0739164828016995,0.135555449614377,
0.049699355361389));
#38806=CARTESIAN_POINT('Ctrl Pts',(0.107036887564708,0.100160226311824,
0.0470514697892497));
#38807=CARTESIAN_POINT('Ctrl Pts',(0.140157292327717,0.0647650030092702,
0.0444035842171104));
#38808=CARTESIAN_POINT('Ctrl Pts',(0.153981866740452,0.0113121504053791,
0.0417556986449711));
#38809=CARTESIAN_POINT('Ctrl Pts',(0.142176802105062,-0.0357014716925755,
0.0391078130728318));
#38810=CARTESIAN_POINT('Ctrl Pts',(0.130371737469673,-0.0827150937905301,
0.0364599275006924));
#38811=CARTESIAN_POINT('Ctrl Pts',(0.0929370337861598,-0.123289485382548,
0.0338120419285532));
#38812=CARTESIAN_POINT('Ctrl Pts',(0.047024206385633,-0.138841291698229,
0.0311641563564138));
#38813=CARTESIAN_POINT('Ctrl Pts',(0.0011113789851062,-0.15439309801391,
0.0285162707842745));
#38814=CARTESIAN_POINT('Ctrl Pts',(-0.0532795721324345,-0.144922319053254,
0.0258683852121352));
#38815=CARTESIAN_POINT('Ctrl Pts',(-0.091223609719915,-0.11475299585383,
0.0232204996399959));
#38816=CARTESIAN_POINT('Ctrl Pts',(-0.125400489590719,-0.0875789416327165,
0.0208355012880941));
#38817=CARTESIAN_POINT('Ctrl Pts',(-0.146234103296486,-0.0436123029244358,
0.0184505029361923));
#38818=CARTESIAN_POINT('Ctrl Pts',(-0.146530139441781,9.2983754875535E-5,
0.0160655045842905));
#38819=CARTESIAN_POINT('Ctrl Pts',(-0.146482381647069,0.000161727750000726,
0.00893449541570906));
#38820=CARTESIAN_POINT('Ctrl Pts',(-0.146143566116611,-0.0424097233364945,
0.0112579996872079));
#38821=CARTESIAN_POINT('Ctrl Pts',(-0.126533645440834,-0.0853716986287587,
0.0135815039587068));
#38822=CARTESIAN_POINT('Ctrl Pts',(-0.0938693583126354,-0.112632000129883,
0.0159050082302056));
#38823=CARTESIAN_POINT('Ctrl Pts',(-0.0566033945712489,-0.143732676025031,
0.0185558429352399));
#38824=CARTESIAN_POINT('Ctrl Pts',(-0.00234583595161722,-0.154396015421179,
0.0212066776402742));
#38825=CARTESIAN_POINT('Ctrl Pts',(0.0439541262059228,-0.139833200290426,
0.0238575123453084));
#38826=CARTESIAN_POINT('Ctrl Pts',(0.0902540883634627,-0.125270385159674,
0.0265083470503427));
#38827=CARTESIAN_POINT('Ctrl Pts',(0.128596454058911,-0.0854814155020214,
0.029159181755377));
#38828=CARTESIAN_POINT('Ctrl Pts',(0.141395806078876,-0.0386806767328055,
0.0318100164604112));
#38829=CARTESIAN_POINT('Ctrl Pts',(0.154195158098842,0.00812006203641059,
0.0344608511654455));
#38830=CARTESIAN_POINT('Ctrl Pts',(0.141451496443324,0.0619325699171903,
0.0371116858704798));
#38831=CARTESIAN_POINT('Ctrl Pts',(0.109005912554766,0.0980207644158424,
0.0397625205755141));
#38832=CARTESIAN_POINT('Ctrl Pts',(0.0765603286662091,0.134108958914494,
0.0424133552805484));
#38833=CARTESIAN_POINT('Ctrl Pts',(0.0244128225446121,0.152472840031019,
0.0450641899855826));
#38834=CARTESIAN_POINT('Ctrl Pts',(-0.0234881253671046,0.144695681732891,
0.0477150246906169));
#38835=CARTESIAN_POINT('Ctrl Pts',(-0.0713890732788212,0.136918523434763,
0.0503658593956511));
#38836=CARTESIAN_POINT('Ctrl Pts',(-0.115043462980658,0.103000325721984,
0.0530166941006854));
#38837=CARTESIAN_POINT('Ctrl Pts',(-0.134410456092164,0.0585065536587812,
0.0556675288057197));
#38838=CARTESIAN_POINT('Ctrl Pts',(-0.142366606622288,0.0402280761403725,
0.0567565176757161));
#38839=CARTESIAN_POINT('Ctrl Pts',(-0.14622390219053,0.0201648150927879,
0.0578455065457126));
#38840=CARTESIAN_POINT('Ctrl Pts',(-0.146138869890956,7.0051777900314E-5,
0.058934495415709));
#38841=CARTESIAN_POINT('Origin',(0.,0.,0.));
#38842=CARTESIAN_POINT('',(-0.146239229308481,-0.000121680145597616,0.116065504584291));
#38843=CARTESIAN_POINT('',(-0.146251911109041,-0.00012571917928438,0.108934495415709));
#38844=CARTESIAN_POINT('',(-0.14635,-1.79227059055215E-17,0.));
#38845=CARTESIAN_POINT('Ctrl Pts',(-0.146239229308481,-0.000121680145597616,
0.116065504584291));
#38846=CARTESIAN_POINT('Ctrl Pts',(-0.145975985392548,0.0334333989639988,
0.114243910896391));
#38847=CARTESIAN_POINT('Ctrl Pts',(-0.134505001919181,0.0671510842014817,
0.112422317208492));
#38848=CARTESIAN_POINT('Ctrl Pts',(-0.113362446108109,0.09293957845923,
0.110600723520593));
#38849=CARTESIAN_POINT('Ctrl Pts',(-0.0826294298146382,0.130425974204838,
0.107952837948454));
#38850=CARTESIAN_POINT('Ctrl Pts',(-0.0314605739124977,0.151158147427946,
0.105304952376314));
#38851=CARTESIAN_POINT('Ctrl Pts',(0.0166981167953111,0.145636463652384,
0.102657066804175));
#38852=CARTESIAN_POINT('Ctrl Pts',(0.0648568075031199,0.140114779876822,
0.100009181232036));
#38853=CARTESIAN_POINT('Ctrl Pts',(0.110005333016597,0.10833923910259,0.0973612956598965));
#38854=CARTESIAN_POINT('Ctrl Pts',(0.1314562431614,0.0648696188566969,0.0947134100877572));
#38855=CARTESIAN_POINT('Ctrl Pts',(0.152907153306203,0.0213999986108032,
0.0920655245156179));
#38856=CARTESIAN_POINT('Ctrl Pts',(0.150660448082332,-0.0337637011067522,
0.0894176389434786));
#38857=CARTESIAN_POINT('Ctrl Pts',(0.125745602608234,-0.075344908113871,
0.0867697533713393));
#38858=CARTESIAN_POINT('Ctrl Pts',(0.100830757134136,-0.11692611512099,
0.0841218677992));
#38859=CARTESIAN_POINT('Ctrl Pts',(0.053247771409812,-0.144924829417672,
0.0814739822270607));
#38860=CARTESIAN_POINT('Ctrl Pts',(0.00479954857812182,-0.146511973337632,
0.0788260966549214));
#38861=CARTESIAN_POINT('Ctrl Pts',(-0.0436486742535683,-0.148099117257592,
0.0761782110827821));
#38862=CARTESIAN_POINT('Ctrl Pts',(-0.0929621341926243,-0.123274690800829,
0.0735303255106428));
#38863=CARTESIAN_POINT('Ctrl Pts',(-0.120544924541891,-0.0834131293658051,
0.0708824399385034));
#38864=CARTESIAN_POINT('Ctrl Pts',(-0.137270788050899,-0.059241570673742,
0.0692767948204325));
#38865=CARTESIAN_POINT('Ctrl Pts',(-0.146006154272575,-0.0295407674383123,
0.0676711497023615));
#38866=CARTESIAN_POINT('Ctrl Pts',(-0.146153148300412,8.02585168747302E-5,
0.0660655045842906));
#38867=CARTESIAN_POINT('Ctrl Pts',(-0.146138869890956,7.0051777900314E-5,
0.058934495415709));
#38868=CARTESIAN_POINT('Ctrl Pts',(-0.14601691516158,-0.0287501898739087,
0.0604963412507468));
#38869=CARTESIAN_POINT('Ctrl Pts',(-0.137785682499354,-0.0576352309664648,
0.0620581870857847));
#38870=CARTESIAN_POINT('Ctrl Pts',(-0.121906950385236,-0.0814126279516829,
0.0636200329208225));
#38871=CARTESIAN_POINT('Ctrl Pts',(-0.0949568550456235,-0.121768691085319,
0.0662708676258568));
#38872=CARTESIAN_POINT('Ctrl Pts',(-0.0459770678452217,-0.147411470938967,
0.068921702330891));
#38873=CARTESIAN_POINT('Ctrl Pts',(0.00254289383979588,-0.146569427669784,
0.0715725370359253));
#38874=CARTESIAN_POINT('Ctrl Pts',(0.0510628555248136,-0.145727384400601,
0.0742233717409596));
#38875=CARTESIAN_POINT('Ctrl Pts',(0.0991229916944473,-0.118400518008588,
0.0768742064459939));
#38876=CARTESIAN_POINT('Ctrl Pts',(0.124657213858417,-0.0771346353870958,
0.0795250411510281));
#38877=CARTESIAN_POINT('Ctrl Pts',(0.150191436022387,-0.0358687527656039,
0.0821758758560624));
#38878=CARTESIAN_POINT('Ctrl Pts',(0.153199744180694,0.0193361460853669,
0.0848267105610966));
#38879=CARTESIAN_POINT('Ctrl Pts',(0.132300679968259,0.0631324945868766,
0.0874775452661308));
#38880=CARTESIAN_POINT('Ctrl Pts',(0.111401615755824,0.106928843088387,
0.0901283799711651));
#38881=CARTESIAN_POINT('Ctrl Pts',(0.0665951791726482,0.139316641240435,
0.0927792146761994));
#38882=CARTESIAN_POINT('Ctrl Pts',(0.0184540622028837,0.145425561817519,
0.0954300493812337));
#38883=CARTESIAN_POINT('Ctrl Pts',(-0.0296870547668806,0.151534482394603,
0.098080884086268));
#38884=CARTESIAN_POINT('Ctrl Pts',(-0.0811628521232332,0.131364525396722,
0.100731718791302));
#38885=CARTESIAN_POINT('Ctrl Pts',(-0.11233861635763,0.0941764269143644,
0.103382553496337));
#38886=CARTESIAN_POINT('Ctrl Pts',(-0.134103588725605,0.0682140181085839,
0.105233200802794));
#38887=CARTESIAN_POINT('Ctrl Pts',(-0.145974404722175,0.0339570340187871,
0.107083848109252));
#38888=CARTESIAN_POINT('Ctrl Pts',(-0.146251911109041,-0.00012571917928438,
0.108934495415709));
#38889=CARTESIAN_POINT('Origin',(0.,0.,0.));
#38890=CARTESIAN_POINT('',(-0.146588437557148,-1.60561805771647E-5,0.166065504584291));
#38891=CARTESIAN_POINT('',(-0.146590338660816,-1.32548991986104E-5,0.158934495415709));
#38892=CARTESIAN_POINT('',(-0.14635,-1.79227059055215E-17,0.));
#38893=CARTESIAN_POINT('Ctrl Pts',(-0.146588437557148,-1.60561805771647E-5,
0.166065504584291));
#38894=CARTESIAN_POINT('Ctrl Pts',(-0.146514434076835,0.0476007616257437,
0.163464557662561));
#38895=CARTESIAN_POINT('Ctrl Pts',(-0.121147481081461,0.0952852365283555,
0.160863610740831));
#38896=CARTESIAN_POINT('Ctrl Pts',(-0.0815892695913163,0.121786698620987,
0.158262663819101));
#38897=CARTESIAN_POINT('Ctrl Pts',(-0.0413171607723027,0.148766426092319,
0.155614778246961));
#38898=CARTESIAN_POINT('Ctrl Pts',(0.0136630407409267,0.153791672495834,
0.152966892674822));
#38899=CARTESIAN_POINT('Ctrl Pts',(0.0581589346640781,0.134559827321239,
0.150319007102683));
#38900=CARTESIAN_POINT('Ctrl Pts',(0.10265482858723,0.115327982146644,0.147671121530543));
#38901=CARTESIAN_POINT('Ctrl Pts',(0.136666414920303,0.0718390453939375,
0.145023235958404));
#38902=CARTESIAN_POINT('Ctrl Pts',(0.144609292620067,0.0240200202446034,
0.142375350386265));
#38903=CARTESIAN_POINT('Ctrl Pts',(0.152552170319831,-0.0237990049047303,
0.139727464814125));
#38904=CARTESIAN_POINT('Ctrl Pts',(0.134426339386286,-0.0759481184506919,
0.137079579241986));
#38905=CARTESIAN_POINT('Ctrl Pts',(0.0985372115045479,-0.108532146892156,
0.134431693669847));
#38906=CARTESIAN_POINT('Ctrl Pts',(0.06264808362281,-0.141116175333621,
0.131783808097708));
#38907=CARTESIAN_POINT('Ctrl Pts',(0.00899565879287956,-0.154135118670589,
0.129135922525568));
#38908=CARTESIAN_POINT('Ctrl Pts',(-0.0378360619111076,-0.141623588974912,
0.126488036953429));
#38909=CARTESIAN_POINT('Ctrl Pts',(-0.0846677826150948,-0.129112059279235,
0.12384015138129));
#38910=CARTESIAN_POINT('Ctrl Pts',(-0.124678799193139,-0.0910700565509135,
0.12119226580915));
#38911=CARTESIAN_POINT('Ctrl Pts',(-0.13953571913976,-0.0449287460526992,
0.118544380237011));
#38912=CARTESIAN_POINT('Ctrl Pts',(-0.144171928689699,-0.0305300156868414,
0.117718088352771));
#38913=CARTESIAN_POINT('Ctrl Pts',(-0.146358639203649,-0.0153425769501271,
0.116891796468531));
#38914=CARTESIAN_POINT('Ctrl Pts',(-0.146239229308481,-0.000121680145597616,
0.116065504584291));
#38915=CARTESIAN_POINT('Ctrl Pts',(-0.146251911109041,-0.00012571917928438,
0.108934495415709));
#38916=CARTESIAN_POINT('Ctrl Pts',(-0.146371899997805,-0.01486250318061,
0.109734682814286));
#38917=CARTESIAN_POINT('Ctrl Pts',(-0.144324466618943,-0.0295667139196708,
0.110534870212863));
#38918=CARTESIAN_POINT('Ctrl Pts',(-0.139972258433256,-0.0435537680369422,
0.111335057611439));
#38919=CARTESIAN_POINT('Ctrl Pts',(-0.125554405162046,-0.0898896245390587,
0.113985892316474));
#38920=CARTESIAN_POINT('Ctrl Pts',(-0.0858429675071836,-0.128355097576459,
0.116636727021508));
#38921=CARTESIAN_POINT('Ctrl Pts',(-0.0390712063381835,-0.141289065177804,
0.119287561726542));
#38922=CARTESIAN_POINT('Ctrl Pts',(0.00770055483081633,-0.15422303277915,
0.121938396431576));
#38923=CARTESIAN_POINT('Ctrl Pts',(0.061532639513954,-0.141625494944442,
0.124589231136611));
#38924=CARTESIAN_POINT('Ctrl Pts',(0.0977084099269336,-0.109280503770194,
0.127240065841645));
#38925=CARTESIAN_POINT('Ctrl Pts',(0.133884180339913,-0.0769355125959451,
0.129890900546679));
#38926=CARTESIAN_POINT('Ctrl Pts',(0.152403636482735,-0.024843068082156,
0.132541735251714));
#38927=CARTESIAN_POINT('Ctrl Pts',(0.144763687764892,0.0230789149168219,
0.135192569956748));
#38928=CARTESIAN_POINT('Ctrl Pts',(0.137123739047049,0.0710008979157997,
0.137843404661782));
#38929=CARTESIAN_POINT('Ctrl Pts',(0.103324385468542,0.114752419399967,
0.140494239366816));
#38930=CARTESIAN_POINT('Ctrl Pts',(0.058884379534592,0.134245263752326,
0.143145074071851));
#38931=CARTESIAN_POINT('Ctrl Pts',(0.0144443736006417,0.153738108104685,
0.145795908776885));
#38932=CARTESIAN_POINT('Ctrl Pts',(-0.0406362846887521,0.148972275325237,
0.148446743481919));
#38933=CARTESIAN_POINT('Ctrl Pts',(-0.0810676758629916,0.122135962547369,
0.151097578186953));
#38934=CARTESIAN_POINT('Ctrl Pts',(-0.120911410803562,0.0956897062586433,
0.153709883929872));
#38935=CARTESIAN_POINT('Ctrl Pts',(-0.146528627904579,0.0478098809758598,
0.15632218967279));
#38936=CARTESIAN_POINT('Ctrl Pts',(-0.146590338660816,-1.32548991986104E-5,
0.158934495415709));
#38937=CARTESIAN_POINT('Origin',(0.,0.,0.));
#38938=CARTESIAN_POINT('',(-0.146286659309134,0.000131086592791319,0.21606550458429));
#38939=CARTESIAN_POINT('',(-0.146291727422766,0.000132510687651112,0.208934495415709));
#38940=CARTESIAN_POINT('',(-0.14635,-1.79227059055215E-17,0.));
#38941=CARTESIAN_POINT('Ctrl Pts',(-0.146286659309134,0.000131086592791319,
0.21606550458429));
#38942=CARTESIAN_POINT('Ctrl Pts',(-0.146403448836959,0.0136116234039521,
0.215333090000869));
#38943=CARTESIAN_POINT('Ctrl Pts',(-0.144693388849564,0.0270630787330369,
0.214600675417447));
#38944=CARTESIAN_POINT('Ctrl Pts',(-0.141038079685752,0.0399633448807191,
0.213868260834026));
#38945=CARTESIAN_POINT('Ctrl Pts',(-0.127823104703478,0.0866014503777888,
0.211220375261887));
#38946=CARTESIAN_POINT('Ctrl Pts',(-0.0891832035626152,0.126035366094718,
0.208572489689747));
#38947=CARTESIAN_POINT('Ctrl Pts',(-0.0428235107164534,0.140196133277333,
0.205924604117608));
#38948=CARTESIAN_POINT('Ctrl Pts',(0.00353618212970767,0.154356900459949,
0.203276718545469));
#38949=CARTESIAN_POINT('Ctrl Pts',(0.0576156666811676,0.143244519108251,
0.200628832973329));
#38950=CARTESIAN_POINT('Ctrl Pts',(0.0946352588096336,0.111950777776248,
0.19798094740119));
#38951=CARTESIAN_POINT('Ctrl Pts',(0.1316548509381,0.0806570364442455,0.195333061829051));
#38952=CARTESIAN_POINT('Ctrl Pts',(0.151614550643572,0.0291819351319375,
0.192685176256911));
#38953=CARTESIAN_POINT('Ctrl Pts',(0.145368652149886,-0.0188881928126718,
0.190037290684772));
#38954=CARTESIAN_POINT('Ctrl Pts',(0.1391227536562,-0.0669583207572802,
0.187389405112633));
#38955=CARTESIAN_POINT('Ctrl Pts',(0.106671256963357,-0.11162347533419,
0.184741519540494));
#38956=CARTESIAN_POINT('Ctrl Pts',(0.06288371648092,-0.132417699194711,
0.182093633968354));
#38957=CARTESIAN_POINT('Ctrl Pts',(0.0190961759984827,-0.153211923055232,
0.179445748396215));
#38958=CARTESIAN_POINT('Ctrl Pts',(-0.0360274082735484,-0.150135216199364,
0.176797862824076));
#38959=CARTESIAN_POINT('Ctrl Pts',(-0.0772289367619549,-0.124597352202288,
0.174149977251936));
#38960=CARTESIAN_POINT('Ctrl Pts',(-0.118430465250361,-0.0990594882052125,
0.171502091679797));
#38961=CARTESIAN_POINT('Ctrl Pts',(-0.145709937955143,-0.0510604670669293,
0.168854206107658));
#38962=CARTESIAN_POINT('Ctrl Pts',(-0.146567666245136,-0.00259385222821292,
0.166206320535519));
#38963=CARTESIAN_POINT('Ctrl Pts',(-0.146582871059412,-0.00173469218203314,
0.166159381885109));
#38964=CARTESIAN_POINT('Ctrl Pts',(-0.146589773079785,-0.000875385198767554,
0.1661124432347));
#38965=CARTESIAN_POINT('Ctrl Pts',(-0.146588437557148,-1.60561805771647E-5,
0.166065504584291));
#38966=CARTESIAN_POINT('Ctrl Pts',(-0.146590338660816,-1.32548991986104E-5,
0.158934495415709));
#38967=CARTESIAN_POINT('Ctrl Pts',(-0.146591248834288,-0.000718599514920206,
0.158973024377825));
#38968=CARTESIAN_POINT('Ctrl Pts',(-0.146586599823099,-0.0014239317987834,
0.15901155333994));
#38969=CARTESIAN_POINT('Ctrl Pts',(-0.146576355279203,-0.00212918280121965,
0.159050082302056));
#38970=CARTESIAN_POINT('Ctrl Pts',(-0.14587151946209,-0.0506512225956504,
0.16170091700709));
#38971=CARTESIAN_POINT('Ctrl Pts',(-0.118679723768778,-0.0987885094082227,
0.164351751712125));
#38972=CARTESIAN_POINT('Ctrl Pts',(-0.0774859020747837,-0.12443912668017,
0.167002586417159));
#38973=CARTESIAN_POINT('Ctrl Pts',(-0.0362920803807891,-0.150089743952118,
0.169653421122193));
#38974=CARTESIAN_POINT('Ctrl Pts',(0.0189037673138887,-0.153253691683441,
0.172304255827227));
#38975=CARTESIAN_POINT('Ctrl Pts',(0.0627588320121262,-0.132478263640569,
0.174955090532262));
#38976=CARTESIAN_POINT('Ctrl Pts',(0.106613896710364,-0.111702835597697,
0.177605925237296));
#38977=CARTESIAN_POINT('Ctrl Pts',(0.139128178412161,-0.0669880317806311,
0.18025675994233));
#38978=CARTESIAN_POINT('Ctrl Pts',(0.14537295917033,-0.0188643595177345,
0.182907594647365));
#38979=CARTESIAN_POINT('Ctrl Pts',(0.151617739928498,0.0292593127451622,
0.185558429352399));
#38980=CARTESIAN_POINT('Ctrl Pts',(0.131593019743037,0.0807918534538889,
0.188209264057433));
#38981=CARTESIAN_POINT('Ctrl Pts',(0.0944930167757219,0.11207243679613,
0.190860098762467));
#38982=CARTESIAN_POINT('Ctrl Pts',(0.0573930138084077,0.143353020138371,
0.193510933467502));
#38983=CARTESIAN_POINT('Ctrl Pts',(0.00321772805924021,0.154381646114126,
0.196161768172536));
#38984=CARTESIAN_POINT('Ctrl Pts',(-0.0431586156002514,0.14009459381994,
0.19881260287757));
#38985=CARTESIAN_POINT('Ctrl Pts',(-0.0895349592597434,0.125807541525753,
0.201463437582605));
#38986=CARTESIAN_POINT('Ctrl Pts',(-0.12811236082956,0.086204810961624,
0.204114272287639));
#38987=CARTESIAN_POINT('Ctrl Pts',(-0.141178260973432,0.0394697345298879,
0.206765106992673));
#38988=CARTESIAN_POINT('Ctrl Pts',(-0.144742548661738,0.0267207271363346,
0.207488236467018));
#38989=CARTESIAN_POINT('Ctrl Pts',(-0.146408370233879,0.0134409584703521,
0.208211365941364));
#38990=CARTESIAN_POINT('Ctrl Pts',(-0.146291727422766,0.000132510687651112,
0.208934495415709));
#38991=CARTESIAN_POINT('Origin',(0.,0.,0.));
#38992=CARTESIAN_POINT('',(-0.146128981728208,-5.54263297282837E-5,0.26606550458429));
#38993=CARTESIAN_POINT('',(-0.146122305401386,-4.76483376818115E-5,0.258934495415709));
#38994=CARTESIAN_POINT('',(-0.14635,-1.79227059055215E-17,0.));
#38995=CARTESIAN_POINT('Ctrl Pts',(-0.146128981728208,-5.54263297282837E-5,
0.26606550458429));
#38996=CARTESIAN_POINT('Ctrl Pts',(-0.146034100463789,0.0278452262029135,
0.264553736767038));
#38997=CARTESIAN_POINT('Ctrl Pts',(-0.138353701663978,0.055794258172635,
0.263041968949786));
#38998=CARTESIAN_POINT('Ctrl Pts',(-0.123420870545114,0.0790954965178402,
0.261530201132533));
#38999=CARTESIAN_POINT('Ctrl Pts',(-0.0972657774021095,0.119907989099794,
0.258882315560394));
#39000=CARTESIAN_POINT('Ctrl Pts',(-0.0488616113353708,0.146461941272529,
0.256234429988255));
#39001=CARTESIAN_POINT('Ctrl Pts',(-0.000387576818673938,0.146590104167151,
0.253586544416116));
#39002=CARTESIAN_POINT('Ctrl Pts',(0.0480864576980232,0.146718267061773,
0.250938658843976));
#39003=CARTESIAN_POINT('Ctrl Pts',(0.0966303606646785,0.120420640678281,
0.248290773271837));
#39004=CARTESIAN_POINT('Ctrl Pts',(0.123000898959779,0.0797470232084743,
0.245642887699697));
#39005=CARTESIAN_POINT('Ctrl Pts',(0.149371437254879,0.0390734057386676,
0.242995002127558));
#39006=CARTESIAN_POINT('Ctrl Pts',(0.153568610878424,-0.0159762028174541,
0.240347116555419));
#39007=CARTESIAN_POINT('Ctrl Pts',(0.133669238840564,-0.0601775991819374,
0.23769923098328));
#39008=CARTESIAN_POINT('Ctrl Pts',(0.113769866802704,-0.104378995546421,
0.235051345411141));
#39009=CARTESIAN_POINT('Ctrl Pts',(0.0697739491034383,-0.137732179719266,
0.232403459839001));
#39010=CARTESIAN_POINT('Ctrl Pts',(0.0218407929672104,-0.144954436352131,
0.229755574266862));
#39011=CARTESIAN_POINT('Ctrl Pts',(-0.0260923631690164,-0.152176692984997,
0.227107688694722));
#39012=CARTESIAN_POINT('Ctrl Pts',(-0.0779627577422058,-0.133268022077883,
0.224459803122583));
#39013=CARTESIAN_POINT('Ctrl Pts',(-0.110002930616958,-0.0968925389857218,
0.221811917550444));
#39014=CARTESIAN_POINT('Ctrl Pts',(-0.133180677518425,-0.0705786441192844,
0.219896446561726));
#39015=CARTESIAN_POINT('Ctrl Pts',(-0.145981221709449,-0.0351243244252332,
0.217980975573008));
#39016=CARTESIAN_POINT('Ctrl Pts',(-0.146286659309134,0.000131086592791319,
0.21606550458429));
#39017=CARTESIAN_POINT('Ctrl Pts',(-0.146291727422766,0.000132510687651112,
0.208934495415709));
#39018=CARTESIAN_POINT('Ctrl Pts',(-0.14598078316578,-0.035344904233501,
0.210862200646398));
#39019=CARTESIAN_POINT('Ctrl Pts',(-0.13300294931328,-0.0710261241835679,
0.212789905877087));
#39020=CARTESIAN_POINT('Ctrl Pts',(-0.109555772823034,-0.0973996609618648,
0.214717611107776));
#39021=CARTESIAN_POINT('Ctrl Pts',(-0.0773129858108336,-0.133666557722538,
0.21736844581281));
#39022=CARTESIAN_POINT('Ctrl Pts',(-0.0252730130685043,-0.152332928944543,
0.220019280517844));
#39023=CARTESIAN_POINT('Ctrl Pts',(0.0226703353838526,-0.144828233467297,
0.222670115222879));
#39024=CARTESIAN_POINT('Ctrl Pts',(0.0706136838362102,-0.137323537990051,
0.225320949927913));
#39025=CARTESIAN_POINT('Ctrl Pts',(0.114460407998596,-0.103647775813554,
0.227971784632947));
#39026=CARTESIAN_POINT('Ctrl Pts',(0.134078573855527,-0.0592629508888991,
0.230622619337982));
#39027=CARTESIAN_POINT('Ctrl Pts',(0.153696739712459,-0.014878125964245,
0.233273454043016));
#39028=CARTESIAN_POINT('Ctrl Pts',(0.149086347263938,0.0402157617085659,
0.23592428874805));
#39029=CARTESIAN_POINT('Ctrl Pts',(0.122364227775469,0.080722717223899,
0.238575123453084));
#39030=CARTESIAN_POINT('Ctrl Pts',(0.0956421082870006,0.121229672739232,
0.241225958158119));
#39031=CARTESIAN_POINT('Ctrl Pts',(0.0468082617585844,0.147149696097087,
0.243876792863153));
#39032=CARTESIAN_POINT('Ctrl Pts',(-0.00171557347725478,0.146581779641701,
0.246527627568187));
#39033=CARTESIAN_POINT('Ctrl Pts',(-0.050239408713094,0.146013863186315,
0.249178462273221));
#39034=CARTESIAN_POINT('Ctrl Pts',(-0.0984532326563563,0.118958006917689,
0.251829296978256));
#39035=CARTESIAN_POINT('Ctrl Pts',(-0.124219986251493,0.0778367286753789,
0.25448013168329));
#39036=CARTESIAN_POINT('Ctrl Pts',(-0.13865248336877,0.054803841451165,
0.255964919594096));
#39037=CARTESIAN_POINT('Ctrl Pts',(-0.146042539478052,0.0273581331787701,
0.257449707504903));
#39038=CARTESIAN_POINT('Ctrl Pts',(-0.146122305401386,-4.76483376818114E-5,
0.258934495415709));
#39039=CARTESIAN_POINT('Origin',(0.,0.,0.));
#39040=CARTESIAN_POINT('',(-0.146489966325848,-0.000104789085069334,0.31606550458429));
#39041=CARTESIAN_POINT('',(-0.146466968003471,-0.000114397412080779,0.308934495415709));
#39042=CARTESIAN_POINT('',(-0.14635,-1.79227059055215E-17,0.));
#39043=CARTESIAN_POINT('Ctrl Pts',(-0.146489966325848,-0.000104789085069334,
0.31606550458429));
#39044=CARTESIAN_POINT('Ctrl Pts',(-0.146149966214897,0.0419143941805715,
0.313774383533207));
#39045=CARTESIAN_POINT('Ctrl Pts',(-0.127114021003857,0.084202434124342,
0.311483262482124));
#39046=CARTESIAN_POINT('Ctrl Pts',(-0.09522591597141,0.111448794443947,
0.309192141431041));
#39047=CARTESIAN_POINT('Ctrl Pts',(-0.0583723183850411,0.142937852758646,
0.306544255858902));
#39048=CARTESIAN_POINT('Ctrl Pts',(-0.00435235065556675,0.154336043577878,
0.303896370286762));
#39049=CARTESIAN_POINT('Ctrl Pts',(0.0420815742217502,0.140420618022043,
0.301248484714623));
#39050=CARTESIAN_POINT('Ctrl Pts',(0.0885154990990669,0.126505192466209,
0.298600599142484));
#39051=CARTESIAN_POINT('Ctrl Pts',(0.127363381124227,0.0872761505353081,
0.295952713570344));
#39052=CARTESIAN_POINT('Ctrl Pts',(0.140824787209621,0.0407085760419468,
0.293304827998205));
#39053=CARTESIAN_POINT('Ctrl Pts',(0.154286193295015,-0.00585899845141487,
0.290656942426066));
#39054=CARTESIAN_POINT('Ctrl Pts',(0.142361123440642,-0.0597651055072374,
0.288009056853927));
#39055=CARTESIAN_POINT('Ctrl Pts',(0.110513747042986,-0.0963095040482439,
0.285361171281788));
#39056=CARTESIAN_POINT('Ctrl Pts',(0.07866637064533,-0.13285390258925,0.282713285709648));
#39057=CARTESIAN_POINT('Ctrl Pts',(0.0268966877043911,-0.152036592615441,
0.280065400137508));
#39058=CARTESIAN_POINT('Ctrl Pts',(-0.0210739885810971,-0.145067900862674,
0.277417514565369));
#39059=CARTESIAN_POINT('Ctrl Pts',(-0.0690446648665853,-0.138099209109907,
0.27476962899323));
#39060=CARTESIAN_POINT('Ctrl Pts',(-0.113216334496623,-0.104979135578184,
0.272121743421091));
#39061=CARTESIAN_POINT('Ctrl Pts',(-0.133349159202006,-0.0608835823167352,
0.269473857848951));
#39062=CARTESIAN_POINT('Ctrl Pts',(-0.141987470405663,-0.0419636782623391,
0.268337740094064));
#39063=CARTESIAN_POINT('Ctrl Pts',(-0.146200286519779,-0.0210232140769756,
0.267201622339177));
#39064=CARTESIAN_POINT('Ctrl Pts',(-0.146128981728208,-5.54263297282837E-5,
0.26606550458429));
#39065=CARTESIAN_POINT('Ctrl Pts',(-0.146122305401386,-4.76483376818114E-5,
0.258934495415709));
#39066=CARTESIAN_POINT('Ctrl Pts',(-0.146184947882857,-0.0215701994360498,
0.260100542209937));
#39067=CARTESIAN_POINT('Ctrl Pts',(-0.141739031650533,-0.0430681260504587,
0.261266589004165));
#39068=CARTESIAN_POINT('Ctrl Pts',(-0.132654825339554,-0.0623847627977247,
0.262432635798393));
#39069=CARTESIAN_POINT('Ctrl Pts',(-0.112003227585469,-0.106298275812525,
0.265083470503427));
#39070=CARTESIAN_POINT('Ctrl Pts',(-0.0673803488302883,-0.138938601626132,
0.267734305208461));
#39071=CARTESIAN_POINT('Ctrl Pts',(-0.019274489346019,-0.145319150065199,
0.270385139913496));
#39072=CARTESIAN_POINT('Ctrl Pts',(0.02883137013825,-0.151699698504265,
0.27303597461853));
#39073=CARTESIAN_POINT('Ctrl Pts',(0.0804202103516079,-0.131820469568792,
0.275686809323564));
#39074=CARTESIAN_POINT('Ctrl Pts',(0.11180535579315,-0.0948088800228575,
0.278337644028599));
#39075=CARTESIAN_POINT('Ctrl Pts',(0.143190501234693,-0.0577972904769225,
0.280988478733633));
#39076=CARTESIAN_POINT('Ctrl Pts',(0.154371951904419,-0.00365334032052542,
0.283639313438667));
#39077=CARTESIAN_POINT('Ctrl Pts',(0.14021581852446,0.0427631330787578,
0.286290148143701));
#39078=CARTESIAN_POINT('Ctrl Pts',(0.126059685144501,0.0891796064780407,
0.288940982848735));
#39079=CARTESIAN_POINT('Ctrl Pts',(0.0865659677148572,0.12786860312021,
0.29159181755377));
#39080=CARTESIAN_POINT('Ctrl Pts',(0.0398679459367864,0.141066325542232,
0.294242652258804));
#39081=CARTESIAN_POINT('Ctrl Pts',(-0.00683007584128473,0.154264047964254,
0.296893486963838));
#39082=CARTESIAN_POINT('Ctrl Pts',(-0.0607324019677826,0.141970496166129,
0.299544321668873));
#39083=CARTESIAN_POINT('Ctrl Pts',(-0.0970901351530201,0.109830173318867,
0.302195156373907));
#39084=CARTESIAN_POINT('Ctrl Pts',(-0.127901447813816,0.0825928994431667,
0.304441602721174));
#39085=CARTESIAN_POINT('Ctrl Pts',(-0.14611277332701,0.0411022848956265,
0.306688049068442));
#39086=CARTESIAN_POINT('Ctrl Pts',(-0.146466968003471,-0.000114397412080779,
0.308934495415709));
#39087=CARTESIAN_POINT('Origin',(0.,0.,0.));
#39088=CARTESIAN_POINT('',(-0.146456696168336,0.00011684297731019,0.36606550458429));
#39089=CARTESIAN_POINT('',(-0.146490622007778,0.000105425447882283,0.358934495415709));
#39090=CARTESIAN_POINT('',(-0.14635,-1.79227059055215E-17,0.));
#39091=CARTESIAN_POINT('Ctrl Pts',(-0.146456696168336,0.00011684297731019,
0.36606550458429));
#39092=CARTESIAN_POINT('Ctrl Pts',(-0.146524266643172,0.00787170677865199,
0.365642915871516));
#39093=CARTESIAN_POINT('Ctrl Pts',(-0.145961554618594,0.0156167466990778,
0.365220327158741));
#39094=CARTESIAN_POINT('Ctrl Pts',(-0.14473428578122,0.0232550097723626,
0.364797738445966));
#39095=CARTESIAN_POINT('Ctrl Pts',(-0.137044379852877,0.0711153666076302,
0.362149852873827));
#39096=CARTESIAN_POINT('Ctrl Pts',(-0.103263231798211,0.11478354525948,
0.359501967301688));
#39097=CARTESIAN_POINT('Ctrl Pts',(-0.0588696551343872,0.134250410014218,
0.356854081729549));
#39098=CARTESIAN_POINT('Ctrl Pts',(-0.0144760784705634,0.153717274768956,
0.354206196157409));
#39099=CARTESIAN_POINT('Ctrl Pts',(0.040529926802418,0.148982825626583,
0.35155831058527));
#39100=CARTESIAN_POINT('Ctrl Pts',(0.0809441375650951,0.122216428534895,
0.34891042501313));
#39101=CARTESIAN_POINT('Ctrl Pts',(0.121358348327771,0.0954500314432082,
0.346262539440991));
#39102=CARTESIAN_POINT('Ctrl Pts',(0.147180764580144,0.0466516864022081,
0.343614653868852));
#39103=CARTESIAN_POINT('Ctrl Pts',(0.146579333092572,-0.00181878629327471,
0.340966768296713));
#39104=CARTESIAN_POINT('Ctrl Pts',(0.145977901604999,-0.0502892589887582,
0.338318882724573));
#39105=CARTESIAN_POINT('Ctrl Pts',(0.11895262237748,-0.0984318593387246,
0.335670997152434));
#39106=CARTESIAN_POINT('Ctrl Pts',(0.0778867105927371,-0.124187234331756,
0.333023111580295));
#39107=CARTESIAN_POINT('Ctrl Pts',(0.036820798807994,-0.149942609324788,
0.330375226008155));
#39108=CARTESIAN_POINT('Ctrl Pts',(-0.0182857455339734,-0.153310758960884,
0.327727340436016));
#39109=CARTESIAN_POINT('Ctrl Pts',(-0.062182630799685,-0.132748368261283,
0.325079454863877));
#39110=CARTESIAN_POINT('Ctrl Pts',(-0.106079516065397,-0.112185977561681,
0.322431569291738));
#39111=CARTESIAN_POINT('Ctrl Pts',(-0.138766742254852,-0.0676930465263806,
0.319783683719598));
#39112=CARTESIAN_POINT('Ctrl Pts',(-0.145266741627948,-0.0196566181036479,
0.317135798147459));
#39113=CARTESIAN_POINT('Ctrl Pts',(-0.146142523114734,-0.0131843998326608,
0.316779033626403));
#39114=CARTESIAN_POINT('Ctrl Pts',(-0.14654290982994,-0.00664785401210523,
0.316422269105347));
#39115=CARTESIAN_POINT('Ctrl Pts',(-0.146489966325848,-0.000104789085069334,
0.31606550458429));
#39116=CARTESIAN_POINT('Ctrl Pts',(-0.146466968003471,-0.000114397412080779,
0.308934495415709));
#39117=CARTESIAN_POINT('Ctrl Pts',(-0.146530727462368,-0.00753391423752658,
0.309338883773476));
#39118=CARTESIAN_POINT('Ctrl Pts',(-0.146015835709215,-0.0149445544285316,
0.309743272131243));
#39119=CARTESIAN_POINT('Ctrl Pts',(-0.144891626709003,-0.0222615773186769,
0.31014766048901));
#39120=CARTESIAN_POINT('Ctrl Pts',(-0.137522244835771,-0.0702259112125575,
0.312798495194044));
#39121=CARTESIAN_POINT('Ctrl Pts',(-0.103970340845329,-0.114167485103918,
0.315449329899078));
#39122=CARTESIAN_POINT('Ctrl Pts',(-0.0596410500115333,-0.133910815353779,
0.318100164604112));
#39123=CARTESIAN_POINT('Ctrl Pts',(-0.015311759177738,-0.15365414560364,
0.320750999309147));
#39124=CARTESIAN_POINT('Ctrl Pts',(0.0397949184994109,-0.149199232212,0.323401834014181));
#39125=CARTESIAN_POINT('Ctrl Pts',(0.0803771156598139,-0.122591519257586,
0.326052668719215));
#39126=CARTESIAN_POINT('Ctrl Pts',(0.120959312820217,-0.0959838063031723,
0.32870350342425));
#39127=CARTESIAN_POINT('Ctrl Pts',(0.147017029463874,-0.0472232937859833,
0.331354338129284));
#39128=CARTESIAN_POINT('Ctrl Pts',(0.146586036983397,0.00130195078264539,
0.334005172834318));
#39129=CARTESIAN_POINT('Ctrl Pts',(0.146155044502921,0.0498271953512744,
0.336656007539352));
#39130=CARTESIAN_POINT('Ctrl Pts',(0.119235342898311,0.0981171719713431,
0.339306842244386));
#39131=CARTESIAN_POINT('Ctrl Pts',(0.0781869354735432,0.123999856599104,
0.341957676949421));
#39132=CARTESIAN_POINT('Ctrl Pts',(0.0371385280487761,0.149882541226865,
0.344608511654455));
#39133=CARTESIAN_POINT('Ctrl Pts',(-0.0180385851961482,0.153357933862318,
0.347259346359489));
#39134=CARTESIAN_POINT('Ctrl Pts',(-0.0620101968435835,0.132830330894432,
0.349910181064524));
#39135=CARTESIAN_POINT('Ctrl Pts',(-0.105981808491019,0.112302727926544,
0.352561015769558));
#39136=CARTESIAN_POINT('Ctrl Pts',(-0.138747918540966,0.0677721293553162,
0.355211850474592));
#39137=CARTESIAN_POINT('Ctrl Pts',(-0.145264183888347,0.0196844656531965,
0.357862685179626));
#39138=CARTESIAN_POINT('Ctrl Pts',(-0.146142422968675,0.0132033812753397,
0.358219955258321));
#39139=CARTESIAN_POINT('Ctrl Pts',(-0.146543841751789,0.00665768391130569,
0.358577225337015));
#39140=CARTESIAN_POINT('Ctrl Pts',(-0.146490622007778,0.000105425447882283,
0.358934495415709));
#39141=CARTESIAN_POINT('Origin',(0.,0.,0.));
#39142=CARTESIAN_POINT('',(-0.146117527463381,3.66422859593568E-5,0.416065504584291));
#39143=CARTESIAN_POINT('',(-0.146131941026353,6.08514395597815E-5,0.408934495415709));
#39144=CARTESIAN_POINT('',(-0.14635,-1.79227059055215E-17,0.));
#39145=CARTESIAN_POINT('Ctrl Pts',(-0.146117527463381,3.66422859593568E-5,
0.416065504584291));
#39146=CARTESIAN_POINT('Ctrl Pts',(-0.146167164015074,0.0222235765819606,
0.414863562637685));
#39147=CARTESIAN_POINT('Ctrl Pts',(-0.141430069804178,0.0443904018142415,
0.413661620691079));
#39148=CARTESIAN_POINT('Ctrl Pts',(-0.131797444393702,0.0641735569006793,
0.412459678744474));
#39149=CARTESIAN_POINT('Ctrl Pts',(-0.11057671079816,0.107755970404684,
0.409811793172335));
#39150=CARTESIAN_POINT('Ctrl Pts',(-0.0655968071821861,0.139769869286095,
0.407163907600195));
#39151=CARTESIAN_POINT('Ctrl Pts',(-0.0174679796227892,0.145546147336919,
0.404516022028056));
#39152=CARTESIAN_POINT('Ctrl Pts',(0.0306608479366084,0.151322425387742,
0.401868136455917));
#39153=CARTESIAN_POINT('Ctrl Pts',(0.0819385994394289,0.130861082607978,
0.399220250883777));
#39154=CARTESIAN_POINT('Ctrl Pts',(0.112869404704651,0.0935377150207321,
0.396572365311638));
#39155=CARTESIAN_POINT('Ctrl Pts',(0.143800209969873,0.0562143474334866,
0.393924479739499));
#39156=CARTESIAN_POINT('Ctrl Pts',(0.154384068997497,0.00202895503876042,
0.391276594167359));
#39157=CARTESIAN_POINT('Ctrl Pts',(0.139771347867625,-0.0441902675604103,
0.38862870859522));
#39158=CARTESIAN_POINT('Ctrl Pts',(0.125158626737753,-0.0904094901595803,
0.385980823023081));
#39159=CARTESIAN_POINT('Ctrl Pts',(0.0853493254503865,-0.128662542963195,
0.383332937450942));
#39160=CARTESIAN_POINT('Ctrl Pts',(0.0385844175605987,-0.141421539587247,
0.380685051878802));
#39161=CARTESIAN_POINT('Ctrl Pts',(-0.00818049032918902,-0.154180536211298,
0.378037166306663));
#39162=CARTESIAN_POINT('Ctrl Pts',(-0.0619010048213979,-0.141445476655787,
0.375389280734523));
#39163=CARTESIAN_POINT('Ctrl Pts',(-0.0979619301664915,-0.109051679368689,
0.372741395162384));
#39164=CARTESIAN_POINT('Ctrl Pts',(-0.128267720099621,-0.081827763001475,
0.370516098303019));
#39165=CARTESIAN_POINT('Ctrl Pts',(-0.146100878890467,-0.0407192549596569,
0.368290801443655));
#39166=CARTESIAN_POINT('Ctrl Pts',(-0.146456696168336,0.00011684297731019,
0.36606550458429));
#39167=CARTESIAN_POINT('Ctrl Pts',(-0.146490622007778,0.000105425447882283,
0.358934495415709));
#39168=CARTESIAN_POINT('Ctrl Pts',(-0.146148967529651,-0.0419580697355662,
0.361228060042049));
#39169=CARTESIAN_POINT('Ctrl Pts',(-0.12707053516474,-0.0842919640484707,
0.363521624668389));
#39170=CARTESIAN_POINT('Ctrl Pts',(-0.0951239884102214,-0.111537384525928,
0.365815189294729));
#39171=CARTESIAN_POINT('Ctrl Pts',(-0.0582011069398996,-0.143026842169921,
0.368466023999764));
#39172=CARTESIAN_POINT('Ctrl Pts',(-0.00408892335444046,-0.154361028624896,
0.371116858704798));
#39173=CARTESIAN_POINT('Ctrl Pts',(0.0423673101370894,-0.140335926848737,
0.373767693409832));
#39174=CARTESIAN_POINT('Ctrl Pts',(0.0888235436286192,-0.126310825072579,
0.376418528114866));
#39175=CARTESIAN_POINT('Ctrl Pts',(0.12762382702622,-0.0869264350652862,
0.379069362819901));
#39176=CARTESIAN_POINT('Ctrl Pts',(0.140953266768128,-0.0402658398230972,
0.381720197524935));
#39177=CARTESIAN_POINT('Ctrl Pts',(0.154282706510036,0.00639475541909176,
0.384371032229969));
#39178=CARTESIAN_POINT('Ctrl Pts',(0.142141302596253,0.0603315558961778,
0.387021866935004));
#39179=CARTESIAN_POINT('Ctrl Pts',(0.110103699587577,0.0967798361409283,
0.389672701640038));
#39180=CARTESIAN_POINT('Ctrl Pts',(0.0780660965789003,0.133228116385679,
0.392323536345072));
#39181=CARTESIAN_POINT('Ctrl Pts',(0.0261322944753315,0.152187876398094,
0.394974371050106));
#39182=CARTESIAN_POINT('Ctrl Pts',(-0.0218526425106493,0.144953866566232,
0.397625205755141));
#39183=CARTESIAN_POINT('Ctrl Pts',(-0.0698375794966294,0.13771985673437,
0.400276040460175));
#39184=CARTESIAN_POINT('Ctrl Pts',(-0.113873651365021,0.104292077058233,
0.402926875165209));
#39185=CARTESIAN_POINT('Ctrl Pts',(-0.133741989653421,0.0600186737328441,
0.405577709870243));
#39186=CARTESIAN_POINT('Ctrl Pts',(-0.142128499086628,0.0413306833614836,
0.406696638385399));
#39187=CARTESIAN_POINT('Ctrl Pts',(-0.14620899575881,0.0207103068323409,
0.407815566900554));
#39188=CARTESIAN_POINT('Ctrl Pts',(-0.146131941026353,6.08514395597814E-5,
0.408934495415709));
#39189=CARTESIAN_POINT('Origin',(0.,0.,0.));
#39190=CARTESIAN_POINT('',(-0.146320034481408,-0.000132042578932776,0.466065504584291));
#39191=CARTESIAN_POINT('',(-0.146267142220666,-0.000128791573925899,0.458934495415709));
#39192=CARTESIAN_POINT('',(-0.14635,-1.79227059055215E-17,0.));
#39193=CARTESIAN_POINT('Ctrl Pts',(-0.146320034481408,-0.000132042578932776,
0.466065504584291));
#39194=CARTESIAN_POINT('Ctrl Pts',(-0.145990955376697,0.0363120653110472,
0.464084209403854));
#39195=CARTESIAN_POINT('Ctrl Pts',(-0.132207444595406,0.0729769481781354,
0.462102914223418));
#39196=CARTESIAN_POINT('Ctrl Pts',(-0.107565849799547,0.0995912952759384,
0.460121619042982));
#39197=CARTESIAN_POINT('Ctrl Pts',(-0.074633794052009,0.135159819536245,
0.457473733470842));
#39198=CARTESIAN_POINT('Ctrl Pts',(-0.0223083694375825,0.15277731788608,
0.454825847898703));
#39199=CARTESIAN_POINT('Ctrl Pts',(0.0254312589463019,0.144368338990174,
0.452177962326564));
#39200=CARTESIAN_POINT('Ctrl Pts',(0.0731708873301868,0.135959360094269,
0.449530076754424));
#39201=CARTESIAN_POINT('Ctrl Pts',(0.116324719483529,0.101523903952622,
0.446882191182285));
#39202=CARTESIAN_POINT('Ctrl Pts',(0.13512098610947,0.0568421509649556,
0.444234305610146));
#39203=CARTESIAN_POINT('Ctrl Pts',(0.153917252735412,0.0121603979772891,
0.441586420038006));
#39204=CARTESIAN_POINT('Ctrl Pts',(0.148355953833953,-0.0427676518563976,
0.438938534465867));
#39205=CARTESIAN_POINT('Ctrl Pts',(0.120984436568095,-0.0827743147100686,
0.436290648893728));
#39206=CARTESIAN_POINT('Ctrl Pts',(0.0936129193022383,-0.122780977563739,
0.433642763321588));
#39207=CARTESIAN_POINT('Ctrl Pts',(0.044431183671984,-0.147866253437395,
0.430994877749449));
#39208=CARTESIAN_POINT('Ctrl Pts',(-0.0040248096733416,-0.146535421965135,
0.42834699217731));
#39209=CARTESIAN_POINT('Ctrl Pts',(-0.0524808030186669,-0.145204590492875,
0.425699106605171));
#39210=CARTESIAN_POINT('Ctrl Pts',(-0.100211054079063,-0.117457651674699,
0.423051221033031));
#39211=CARTESIAN_POINT('Ctrl Pts',(-0.125345397821707,-0.0760087182023128,
0.420403335460892));
#39212=CARTESIAN_POINT('Ctrl Pts',(-0.139070629946179,-0.0533744994995956,
0.418957391835358));
#39213=CARTESIAN_POINT('Ctrl Pts',(-0.146057814383464,-0.0266543774475973,
0.417511448209824));
#39214=CARTESIAN_POINT('Ctrl Pts',(-0.146117527463381,3.66422859593568E-5,
0.416065504584291));
#39215=CARTESIAN_POINT('Ctrl Pts',(-0.146131941026353,6.08514395597814E-5,
0.408934495415709));
#39216=CARTESIAN_POINT('Ctrl Pts',(-0.146026446689573,-0.0282099702486701,
0.410466401605588));
#39217=CARTESIAN_POINT('Ctrl Pts',(-0.138128084958642,-0.0565352970304639,
0.411998307795467));
#39218=CARTESIAN_POINT('Ctrl Pts',(-0.122817836477901,-0.0800308731172956,
0.413530213985346));
#39219=CARTESIAN_POINT('Ctrl Pts',(-0.0963247403055724,-0.120687989667408,
0.41618104869038));
#39220=CARTESIAN_POINT('Ctrl Pts',(-0.0476379432525075,-0.146883195792991,
0.418831883395415));
#39221=CARTESIAN_POINT('Ctrl Pts',(0.000888321221429993,-0.146589129065305,
0.421482718100449));
#39222=CARTESIAN_POINT('Ctrl Pts',(0.0494145856953668,-0.146295062337618,
0.424133552805483));
#39223=CARTESIAN_POINT('Ctrl Pts',(0.097780317590176,-0.119511722756663,
0.426784387510517));
#39224=CARTESIAN_POINT('Ctrl Pts',(0.123778732978107,-0.0785365161302261,
0.429435222215552));
#39225=CARTESIAN_POINT('Ctrl Pts',(0.149777148366038,-0.0375613095037888,
0.432086056920586));
#39226=CARTESIAN_POINT('Ctrl Pts',(0.15340824724709,0.0176057641681304,
0.43473689162562));
#39227=CARTESIAN_POINT('Ctrl Pts',(0.13300479146532,0.0616351303104708,
0.437387726330655));
#39228=CARTESIAN_POINT('Ctrl Pts',(0.112601335683551,0.105664496452811,
0.440038561035689));
#39229=CARTESIAN_POINT('Ctrl Pts',(0.0681633252389606,0.138556155065572,
0.442689395740723));
#39230=CARTESIAN_POINT('Ctrl Pts',(0.0200942611983476,0.145208074081285,
0.445340230445757));
#39231=CARTESIAN_POINT('Ctrl Pts',(-0.0279748028422658,0.151859993096997,
0.447991065150791));
#39232=CARTESIAN_POINT('Ctrl Pts',(-0.0796749204789013,0.132272172515661,
0.450641899855826));
#39233=CARTESIAN_POINT('Ctrl Pts',(-0.111268479500082,0.095438314693151,
0.45329273456086));
#39234=CARTESIAN_POINT('Ctrl Pts',(-0.133681961086661,0.0693071974766942,
0.455173321512477));
#39235=CARTESIAN_POINT('Ctrl Pts',(-0.145975937294016,0.0344962574238126,
0.457053908464093));
#39236=CARTESIAN_POINT('Ctrl Pts',(-0.146267142220666,-0.000128791573925899,
0.458934495415709));
#39237=CARTESIAN_POINT('Origin',(0.,0.,-0.0924367114736154));
#39238=CARTESIAN_POINT('',(-0.117750885282186,-0.00010626111879085,0.482563288526385));
#39239=CARTESIAN_POINT('',(-0.117972864089022,-5.93608753193428E-7,0.492436711473616));
#39240=CARTESIAN_POINT('',(-0.117775,-8.88924268665971E-15,-0.0924367114736154));
#39241=CARTESIAN_POINT('',(-0.117668597464311,0.00500517689817391,0.532225000000001));
#39242=CARTESIAN_POINT('Ctrl Pts',(-0.117750885282186,-0.000106261118790843,
0.482563288526385));
#39243=CARTESIAN_POINT('Ctrl Pts',(-0.117839983816431,-0.00997354393438475,
0.483229878918088));
#39244=CARTESIAN_POINT('Ctrl Pts',(-0.112189023051801,-0.0589364681957879,
0.486544354881929));
#39245=CARTESIAN_POINT('Ctrl Pts',(-0.0439766578214066,-0.132120623957634,
0.492506716417911));
#39246=CARTESIAN_POINT('Ctrl Pts',(0.087240331747497,-0.108512430051717,
0.500450373134329));
#39247=CARTESIAN_POINT('Ctrl Pts',(0.138438921804208,0.0144739368962113,
0.508394029850746));
#39248=CARTESIAN_POINT('Ctrl Pts',(0.0629040591690992,0.12431971381125,
0.516337686567165));
#39249=CARTESIAN_POINT('Ctrl Pts',(-0.0705459363093062,0.119993110375402,
0.524281343283582));
#39250=CARTESIAN_POINT('Ctrl Pts',(-0.116003159314893,0.0441585924901374,
0.529577114427861));
#39251=CARTESIAN_POINT('Ctrl Pts',(-0.117668597464311,0.00500517689817385,
0.532225));
#39252=CARTESIAN_POINT('',(-0.0334019664626897,0.112939183906319,0.532225000000001));
#39253=CARTESIAN_POINT('Origin',(0.,0.,0.532225));
#39254=CARTESIAN_POINT('Ctrl Pts',(-0.117972864533492,-5.93610086620396E-7,
0.492436711473617));
#39255=CARTESIAN_POINT('Ctrl Pts',(-0.117972892941239,-0.000127136793190444,
0.492445300790573));
#39256=CARTESIAN_POINT('Ctrl Pts',(-0.117912463615216,-0.0393074137896712,
0.495104724812564));
#39257=CARTESIAN_POINT('Ctrl Pts',(-0.0749307309976486,-0.117412744486246,
0.500414983539588));
#39258=CARTESIAN_POINT('Ctrl Pts',(0.0581614397283287,-0.126517333775439,
0.508367487654693));
#39259=CARTESIAN_POINT('Ctrl Pts',(0.138005962114904,-0.01953005209576,
0.516319991769794));
#39260=CARTESIAN_POINT('Ctrl Pts',(0.0908022345067483,0.105567300931769,
0.524272495884898));
#39261=CARTESIAN_POINT('Ctrl Pts',(0.00421962447768953,0.124065836989857,
0.529574165294966));
#39262=CARTESIAN_POINT('Ctrl Pts',(-0.0334019664626881,0.11293918390632,
0.532225));
#39263=CARTESIAN_POINT('Origin',(0.,0.,-0.0924367114736154));
#39264=CARTESIAN_POINT('',(-0.117587917984282,2.94878389348885E-5,0.432563288526385));
#39265=CARTESIAN_POINT('',(-0.117708320294082,-0.000103644876124687,0.442436711473616));
#39266=CARTESIAN_POINT('',(-0.117775,-8.88924268665971E-15,-0.0924367114736154));
#39267=CARTESIAN_POINT('Ctrl Pts',(-0.117587917984282,2.94878389348868E-5,
0.432563288526385));
#39268=CARTESIAN_POINT('Ctrl Pts',(-0.117539863949521,-0.0214500806552194,
0.434009232151918));
#39269=CARTESIAN_POINT('Ctrl Pts',(-0.101619941365326,-0.082330436444606,
0.438103061349591));
#39270=CARTESIAN_POINT('Ctrl Pts',(-0.00382300141363195,-0.139182551176009,
0.444844776119403));
#39271=CARTESIAN_POINT('Ctrl Pts',(0.11491384000461,-0.0786205074584852,
0.452788432835821));
#39272=CARTESIAN_POINT('Ctrl Pts',(0.128340187352459,0.0539893538840985,
0.460732089552239));
#39273=CARTESIAN_POINT('Ctrl Pts',(0.024156191824071,0.137125039167645,
0.468675746268657));
#39274=CARTESIAN_POINT('Ctrl Pts',(-0.0915696283436722,0.0981611996792526,
0.475952812593373));
#39275=CARTESIAN_POINT('Ctrl Pts',(-0.117486059238065,0.0292220942398885,
0.480581993345948));
#39276=CARTESIAN_POINT('Ctrl Pts',(-0.117750885282186,-0.000106261118790843,
0.482563288526385));
#39277=CARTESIAN_POINT('Ctrl Pts',(-0.117708320294082,-0.000103644876124676,
0.442436711473616));
#39278=CARTESIAN_POINT('Ctrl Pts',(-0.117804303693274,-0.0115163291952777,
0.443206959227034));
#39279=CARTESIAN_POINT('Ctrl Pts',(-0.111033657777347,-0.0620947057757177,
0.446628041685486));
#39280=CARTESIAN_POINT('Ctrl Pts',(-0.038636663810782,-0.133821400192823,
0.452699958848972));
#39281=CARTESIAN_POINT('Ctrl Pts',(0.0916608011058181,-0.104875817685159,
0.460652462964076));
#39282=CARTESIAN_POINT('Ctrl Pts',(0.137790741908166,0.0203740232160909,
0.468604967079177));
#39283=CARTESIAN_POINT('Ctrl Pts',(0.0573828398023632,0.126918127906013,
0.476557471194281));
#39284=CARTESIAN_POINT('Ctrl Pts',(-0.0755630108222985,0.116919225220885,
0.484501385992427));
#39285=CARTESIAN_POINT('Ctrl Pts',(-0.117964125743295,0.0389266160426656,
0.489794466085539));
#39286=CARTESIAN_POINT('Ctrl Pts',(-0.117972864533492,-5.93610086620396E-7,
0.492436711473617));
#39287=CARTESIAN_POINT('Origin',(0.,0.,-0.0924367114736154));
#39288=CARTESIAN_POINT('',(-0.117860863622998,9.40292562467743E-5,0.382563288526384));
#39289=CARTESIAN_POINT('',(-0.11759951728308,4.89701284099239E-5,0.392436711473616));
#39290=CARTESIAN_POINT('',(-0.117775,-8.88924268665971E-15,-0.0924367114736154));
#39291=CARTESIAN_POINT('Ctrl Pts',(-0.117860863622998,9.40292562467788E-5,
0.382563288526384));
#39292=CARTESIAN_POINT('Ctrl Pts',(-0.117574520063714,-0.0327687752160871,
0.384788585385749));
#39293=CARTESIAN_POINT('Ctrl Pts',(-0.0861467637051906,-0.105215176336211,
0.389661767817253));
#39294=CARTESIAN_POINT('Ctrl Pts',(0.0366482838797405,-0.134325140358292,
0.397182835820896));
#39295=CARTESIAN_POINT('Ctrl Pts',(0.132757756905765,-0.0419728350502109,
0.405126492537314));
#39296=CARTESIAN_POINT('Ctrl Pts',(0.107205710503746,0.0888440680441954,
0.413070149253731));
#39297=CARTESIAN_POINT('Ctrl Pts',(-0.0165914302528927,0.138242796692368,
0.42101380597015));
#39298=CARTESIAN_POINT('Ctrl Pts',(-0.105417454577164,0.0750219551131263,
0.427511519061034));
#39299=CARTESIAN_POINT('Ctrl Pts',(-0.117627862944144,0.0178843985783384,
0.431361346579779));
#39300=CARTESIAN_POINT('Ctrl Pts',(-0.117587917984282,2.94878389348868E-5,
0.432563288526385));
#39301=CARTESIAN_POINT('Ctrl Pts',(-0.11759951728308,4.89701284099274E-5,
0.392436711473616));
#39302=CARTESIAN_POINT('Ctrl Pts',(-0.11751462083269,-0.0227019422346301,
0.393968617663495));
#39303=CARTESIAN_POINT('Ctrl Pts',(-0.100159557717256,-0.0849411572528722,
0.398151358558408));
#39304=CARTESIAN_POINT('Ctrl Pts',(0.000844063931402275,-0.139284651766041,
0.404984934158356));
#39305=CARTESIAN_POINT('Ctrl Pts',(0.117610871049501,-0.0746230633995127,
0.412937438273457));
#39306=CARTESIAN_POINT('Ctrl Pts',(0.126377239427685,0.0585638604483229,
0.420889942388562));
#39307=CARTESIAN_POINT('Ctrl Pts',(0.0190929207373193,0.137972437690235,
0.428842446503664));
#39308=CARTESIAN_POINT('Ctrl Pts',(-0.0936346562739906,0.0952629110198009,
0.436024702865349));
#39309=CARTESIAN_POINT('Ctrl Pts',(-0.117473973452704,0.0277608248588199,
0.440556124522));
#39310=CARTESIAN_POINT('Ctrl Pts',(-0.117708320294082,-0.000103644876124676,
0.442436711473616));
#39311=CARTESIAN_POINT('Origin',(0.,0.,-0.0924367114736154));
#39312=CARTESIAN_POINT('',(-0.117887637745315,-8.43288998643762E-5,0.332563288526385));
#39313=CARTESIAN_POINT('',(-0.11788816540462,8.48410121138156E-5,0.342436711473616));
#39314=CARTESIAN_POINT('',(-0.117775,-8.88924268665971E-15,-0.0924367114736154));
#39315=CARTESIAN_POINT('Ctrl Pts',(-0.117887637745315,-8.43288998643547E-5,
0.332563288526385));
#39316=CARTESIAN_POINT('Ctrl Pts',(-0.117930243971446,-0.00534985313478999,
0.332920053047441));
#39317=CARTESIAN_POINT('Ctrl Pts',(-0.115216603610867,-0.0496516091215746,
0.335924703140636));
#39318=CARTESIAN_POINT('Ctrl Pts',(-0.0590623637863932,-0.126087177724698,
0.34157723880597));
#39319=CARTESIAN_POINT('Ctrl Pts',(0.0739784273282333,-0.117955633685244,
0.349520895522388));
#39320=CARTESIAN_POINT('Ctrl Pts',(0.139224117680559,-0.00172752115601949,
0.357464552238807));
#39321=CARTESIAN_POINT('Ctrl Pts',(0.0768824352591712,0.11608372080921,
0.365408208955224));
#39322=CARTESIAN_POINT('Ctrl Pts',(-0.0559156297430559,0.12751384888047,
0.373351865671643));
#39323=CARTESIAN_POINT('Ctrl Pts',(-0.114624951070718,0.0516215456314347,
0.379070225528695));
#39324=CARTESIAN_POINT('Ctrl Pts',(-0.117915240887596,0.00633474728975054,
0.382140699813609));
#39325=CARTESIAN_POINT('Ctrl Pts',(-0.117860863622998,9.40292562467788E-5,
0.382563288526384));
#39326=CARTESIAN_POINT('Ctrl Pts',(-0.11788816540462,8.4841012113826E-5,
0.342436711473616));
#39327=CARTESIAN_POINT('Ctrl Pts',(-0.1176132193427,-0.0337657100314819,
0.344730276099956));
#39328=CARTESIAN_POINT('Ctrl Pts',(-0.0845149237619996,-0.107208837865588,
0.34967467543133));
#39329=CARTESIAN_POINT('Ctrl Pts',(0.0402561631274929,-0.133343040355529,
0.357269909467738));
#39330=CARTESIAN_POINT('Ctrl Pts',(0.133929618074243,-0.0382594079720193,
0.365222413582842));
#39331=CARTESIAN_POINT('Ctrl Pts',(0.104617274119081,0.0919573329132998,
0.373174917697944));
#39332=CARTESIAN_POINT('Ctrl Pts',(-0.020763734615072,0.137730870367254,
0.381127421813047));
#39333=CARTESIAN_POINT('Ctrl Pts',(-0.106598215372521,0.0725739208566139,
0.387548019738271));
#39334=CARTESIAN_POINT('Ctrl Pts',(-0.117661526993468,0.0166665964275914,
0.391317782958461));
#39335=CARTESIAN_POINT('Ctrl Pts',(-0.11759951728308,4.89701284099274E-5,
0.392436711473616));
#39336=CARTESIAN_POINT('Origin',(0.,0.,-0.0924367114736154));
#39337=CARTESIAN_POINT('',(-0.117597135791184,-4.46042773137295E-5,0.282563288526384));
#39338=CARTESIAN_POINT('',(-0.117869129870917,-9.20611903598989E-5,0.292436711473616));
#39339=CARTESIAN_POINT('',(-0.117775,-8.88924268665971E-15,-0.0924367114736154));
#39340=CARTESIAN_POINT('Ctrl Pts',(-0.117597135791184,-4.46042773137294E-5,
0.282563288526384));
#39341=CARTESIAN_POINT('Ctrl Pts',(-0.117654518243026,-0.0169184081852861,
0.283699406281271));
#39342=CARTESIAN_POINT('Ctrl Pts',(-0.106362773508523,-0.0730457989372372,
0.287483409608297));
#39343=CARTESIAN_POINT('Ctrl Pts',(-0.0200165152988323,-0.137788527592198,
0.293915298507463));
#39344=CARTESIAN_POINT('Ctrl Pts',(0.104968269293632,-0.0914767820950745,
0.301858955223881));
#39345=CARTESIAN_POINT('Ctrl Pts',(0.133758329466478,0.0386658573002006,
0.309802611940298));
#39346=CARTESIAN_POINT('Ctrl Pts',(0.0399699596916912,0.133374441107753,
0.317746268656717));
#39347=CARTESIAN_POINT('Ctrl Pts',(-0.084590271720082,0.107092283864913,
0.325333160852078));
#39348=CARTESIAN_POINT('Ctrl Pts',(-0.117614023033548,0.0337305621770822,
0.330272167475301));
#39349=CARTESIAN_POINT('Ctrl Pts',(-0.117887637745315,-8.43288998643547E-5,
0.332563288526385));
#39350=CARTESIAN_POINT('Ctrl Pts',(-0.117869129870917,-9.2061190359885E-5,
0.292436711473616));
#39351=CARTESIAN_POINT('Ctrl Pts',(-0.117920440224669,-0.00606290911736031,
0.292841099831383));
#39352=CARTESIAN_POINT('Ctrl Pts',(-0.114789890532149,-0.0511197142210238,
0.295896322894184));
#39353=CARTESIAN_POINT('Ctrl Pts',(-0.0566691588697243,-0.127238089669758,
0.301602380662019));
#39354=CARTESIAN_POINT('Ctrl Pts',(0.0763719541489209,-0.116482829853556,
0.309554884777122));
#39355=CARTESIAN_POINT('Ctrl Pts',(0.139281709756163,0.00123707506708643,
0.317507388892225));
#39356=CARTESIAN_POINT('Ctrl Pts',(0.0742909098282569,0.117820990265484,
0.325459893007327));
#39357=CARTESIAN_POINT('Ctrl Pts',(-0.0589202520252667,0.1262114453589,
0.33341239712243));
#39358=CARTESIAN_POINT('Ctrl Pts',(-0.115211084829427,0.0497097039247984,
0.339071336611193));
#39359=CARTESIAN_POINT('Ctrl Pts',(-0.11793099393452,0.00535776373524371,
0.342079441394922));
#39360=CARTESIAN_POINT('Ctrl Pts',(-0.11788816540462,8.4841012113826E-5,
0.342436711473616));
#39361=CARTESIAN_POINT('Origin',(0.,0.,-0.0924367114736154));
#39362=CARTESIAN_POINT('',(-0.117724026649356,0.00010549178999148,0.232563288526384));
#39363=CARTESIAN_POINT('',(-0.117591763024586,-3.83449468523145E-5,0.242436711473616));
#39364=CARTESIAN_POINT('',(-0.117775,-8.88924268665971E-15,-0.0924367114736154));
#39365=CARTESIAN_POINT('Ctrl Pts',(-0.117724026649356,0.000105491789991495,
0.232563288526384));
#39366=CARTESIAN_POINT('Ctrl Pts',(-0.117478226080151,-0.0282662610808501,
0.234478759515102));
#39367=CARTESIAN_POINT('Ctrl Pts',(-0.0929369215417509,-0.0962395631396471,
0.239042116075959));
#39368=CARTESIAN_POINT('Ctrl Pts',(0.0207448421498254,-0.137680756627218,
0.246253358208955));
#39369=CARTESIAN_POINT('Ctrl Pts',(0.126961839902422,-0.0571579428392388,
0.254197014925373));
#39370=CARTESIAN_POINT('Ctrl Pts',(0.116828827462796,0.075745391244066,
0.262140671641791));
#39371=CARTESIAN_POINT('Ctrl Pts',(-0.000368128572008151,0.139234348141551,
0.270084328358209));
#39372=CARTESIAN_POINT('Ctrl Pts',(-0.100514230788311,0.0842953826634335,
0.27689186731974));
#39373=CARTESIAN_POINT('Ctrl Pts',(-0.117520780198996,0.0224084148687892,
0.281051520709132));
#39374=CARTESIAN_POINT('Ctrl Pts',(-0.117597135791184,-4.46042773137294E-5,
0.282563288526384));
#39375=CARTESIAN_POINT('Ctrl Pts',(-0.117591763024586,-3.83449468523075E-5,
0.242436711473616));
#39376=CARTESIAN_POINT('Ctrl Pts',(-0.117642174491994,-0.017358594045656,
0.243602758267844));
#39377=CARTESIAN_POINT('Ctrl Pts',(-0.10593062496396,-0.0739889980249599,
0.247419639767106));
#39378=CARTESIAN_POINT('Ctrl Pts',(-0.0183140487741412,-0.138077951344142,
0.253887355971402));
#39379=CARTESIAN_POINT('Ctrl Pts',(0.106234136865658,-0.0900845891054932,
0.261839860086505));
#39380=CARTESIAN_POINT('Ctrl Pts',(0.133228916899009,0.040632262203075,
0.269792364201608));
#39381=CARTESIAN_POINT('Ctrl Pts',(0.0378813411502606,0.134037043471229,
0.27774486831671));
#39382=CARTESIAN_POINT('Ctrl Pts',(-0.085634823441202,0.105866601183683,
0.285292984074047));
#39383=CARTESIAN_POINT('Ctrl Pts',(-0.117584092098319,0.0330770181317487,
0.290190265126349));
#39384=CARTESIAN_POINT('Ctrl Pts',(-0.117869129870917,-9.2061190359885E-5,
0.292436711473616));
#39385=CARTESIAN_POINT('Origin',(0.,0.,-0.0924367114736154));
#39386=CARTESIAN_POINT('',(-0.117966882359366,-1.29211934964908E-5,0.182563288526384));
#39387=CARTESIAN_POINT('',(-0.117728105208174,0.000106637828744482,0.192436711473616));
#39388=CARTESIAN_POINT('',(-0.117775,-8.88924268665971E-15,-0.0924367114736154));
#39389=CARTESIAN_POINT('Ctrl Pts',(-0.117966882359366,-1.29211934964912E-5,
0.182563288526384));
#39390=CARTESIAN_POINT('Ctrl Pts',(-0.117967957119725,-0.000704465266726215,
0.182610227176794));
#39391=CARTESIAN_POINT('Ctrl Pts',(-0.117649070375187,-0.0404061166150831,
0.185305051399342));
#39392=CARTESIAN_POINT('Ctrl Pts',(-0.0733536600413758,-0.118345172107485,
0.19064776119403));
#39393=CARTESIAN_POINT('Ctrl Pts',(0.0597282696676458,-0.12577310138558,
0.198591417910448));
#39394=CARTESIAN_POINT('Ctrl Pts',(0.138074187460599,-0.0179404007303906,
0.206535074626866));
#39395=CARTESIAN_POINT('Ctrl Pts',(0.0898865489335327,0.106333191146418,
0.214478731343283));
#39396=CARTESIAN_POINT('Ctrl Pts',(-0.0406746665030564,0.133161220808791,
0.222422388059702));
#39397=CARTESIAN_POINT('Ctrl Pts',(-0.111466604862902,0.0609145729578186,
0.228450573787402));
#39398=CARTESIAN_POINT('Ctrl Pts',(-0.117818012892196,0.0109539388206346,
0.231830873942963));
#39399=CARTESIAN_POINT('Ctrl Pts',(-0.117724026649356,0.000105491789991495,
0.232563288526384));
#39400=CARTESIAN_POINT('Ctrl Pts',(-0.117728105208174,0.000106637828744488,
0.192436711473616));
#39401=CARTESIAN_POINT('Ctrl Pts',(-0.11747787316262,-0.0284437724366353,
0.194364416704305));
#39402=CARTESIAN_POINT('Ctrl Pts',(-0.0926723165398222,-0.0966441001570621,
0.198942956640028));
#39403=CARTESIAN_POINT('Ctrl Pts',(0.0215406810767683,-0.137611496939632,
0.206172331280785));
#39404=CARTESIAN_POINT('Ctrl Pts',(0.127397488829925,-0.056309900280862,
0.214124835395888));
#39405=CARTESIAN_POINT('Ctrl Pts',(0.116266864218555,0.0767003345124148,
0.222077339510991));
#39406=CARTESIAN_POINT('Ctrl Pts',(-0.0016300870944122,0.139277664563073,
0.230029843626094));
#39407=CARTESIAN_POINT('Ctrl Pts',(-0.100962832358778,0.0835357163242542,
0.236816300946969));
#39408=CARTESIAN_POINT('Ctrl Pts',(-0.117527571486354,0.0220164272984534,
0.240951923562809));
#39409=CARTESIAN_POINT('Ctrl Pts',(-0.117591763024586,-3.83449468523075E-5,
0.242436711473616));
#39410=CARTESIAN_POINT('Origin',(0.,0.,-0.0924367114736154));
#39411=CARTESIAN_POINT('',(-0.117685857408994,-9.79219620674319E-5,0.132563288526384));
#39412=CARTESIAN_POINT('',(-0.117968412270431,-1.06668654225733E-5,0.142436711473616));
#39413=CARTESIAN_POINT('',(-0.117775,-8.88924268665971E-15,-0.0924367114736154));
#39414=CARTESIAN_POINT('Ctrl Pts',(-0.117685857408994,-9.79219620674231E-5,
0.132563288526384));
#39415=CARTESIAN_POINT('Ctrl Pts',(-0.117781952389543,-0.0123469217649596,
0.133389580410625));
#39416=CARTESIAN_POINT('Ctrl Pts',(-0.110383000729775,-0.063735125339128,
0.136863757867004));
#39417=CARTESIAN_POINT('Ctrl Pts',(-0.03593748288359,-0.134517045800752,
0.142985820895522));
#39418=CARTESIAN_POINT('Ctrl Pts',(0.0935927050428541,-0.103086105216301,
0.150929477611941));
#39419=CARTESIAN_POINT('Ctrl Pts',(0.137352931996012,0.0228147184504364,
0.158873134328358));
#39420=CARTESIAN_POINT('Ctrl Pts',(0.0552405729858772,0.127807739141585,
0.166816791044776));
#39421=CARTESIAN_POINT('Ctrl Pts',(-0.0767108666901454,0.115747243191764,
0.174713509110785));
#39422=CARTESIAN_POINT('Ctrl Pts',(-0.117907328140755,0.0383066600647174,
0.179962341604654));
#39423=CARTESIAN_POINT('Ctrl Pts',(-0.117966882359366,-1.29211934964912E-5,
0.182563288526384));
#39424=CARTESIAN_POINT('Ctrl Pts',(-0.117968412270431,-1.06668654225827E-5,
0.142436711473616));
#39425=CARTESIAN_POINT('Ctrl Pts',(-0.117969144731522,-0.000578292161741028,
0.142475240435732));
#39426=CARTESIAN_POINT('Ctrl Pts',(-0.117707998838203,-0.0401984655398319,
0.145164604102881));
#39427=CARTESIAN_POINT('Ctrl Pts',(-0.0736248085349355,-0.118238371369349,
0.150504802475065));
#39428=CARTESIAN_POINT('Ctrl Pts',(0.0596315829014974,-0.125876921640408,
0.158457306590168));
#39429=CARTESIAN_POINT('Ctrl Pts',(0.138129079193178,-0.0179243554725553,
0.166409810705271));
#39430=CARTESIAN_POINT('Ctrl Pts',(0.0897844651888838,0.106487909275724,
0.174362314820374));
#39431=CARTESIAN_POINT('Ctrl Pts',(-0.0410080379701501,0.133113732800722,
0.182314818935477));
#39432=CARTESIAN_POINT('Ctrl Pts',(-0.111567175621,0.0606792399755161,0.188339617819891));
#39433=CARTESIAN_POINT('Ctrl Pts',(-0.117821973380904,0.0108165964048154,
0.19171358199927));
#39434=CARTESIAN_POINT('Ctrl Pts',(-0.117728105208174,0.000106637828744488,
0.192436711473616));
#39435=CARTESIAN_POINT('Origin',(0.,0.,-0.0924367114736154));
#39436=CARTESIAN_POINT('',(-0.117616583813332,6.45879523355414E-5,0.0825632885263843));
#39437=CARTESIAN_POINT('',(-0.117696063073914,-0.000101172369946279,0.092436711473616));
#39438=CARTESIAN_POINT('',(-0.117775,-8.88924268665971E-15,-0.0924367114736154));
#39439=CARTESIAN_POINT('Ctrl Pts',(-0.117616583813332,6.4587952335533E-5,
0.0825632885263843));
#39440=CARTESIAN_POINT('Ctrl Pts',(-0.117498290532644,-0.023772899795338,
0.0841689336444552));
#39441=CARTESIAN_POINT('Ctrl Pts',(-0.0988756392612849,-0.087091103874762,
0.0884224643346654));
#39442=CARTESIAN_POINT('Ctrl Pts',(0.00455872999049264,-0.139160029798142,
0.0953238805970148));
#39443=CARTESIAN_POINT('Ctrl Pts',(0.119435794773867,-0.0715642270726515,
0.103267537313433));
#39444=CARTESIAN_POINT('Ctrl Pts',(0.124859895376695,0.0616145512171006,
0.111211194029851));
#39445=CARTESIAN_POINT('Ctrl Pts',(0.0158602180480347,0.138328544685192,
0.119154850746269));
#39446=CARTESIAN_POINT('Ctrl Pts',(-0.094824103560013,0.0934823880103396,
0.126272215578446));
#39447=CARTESIAN_POINT('Ctrl Pts',(-0.117474012159943,0.0269054906934358,
0.130741694838485));
#39448=CARTESIAN_POINT('Ctrl Pts',(-0.117685857408994,-9.79219620674231E-5,
0.132563288526384));
#39449=CARTESIAN_POINT('Ctrl Pts',(-0.117696063073914,-0.000101172369946261,
0.092436711473616));
#39450=CARTESIAN_POINT('Ctrl Pts',(-0.117792623998916,-0.0119605829319943,
0.0932368988721926));
#39451=CARTESIAN_POINT('Ctrl Pts',(-0.110686607712821,-0.0629944099979452,
0.0966879209758034));
#39452=CARTESIAN_POINT('Ctrl Pts',(-0.0371242974264225,-0.134248668971966,
0.102789777784449));
#39453=CARTESIAN_POINT('Ctrl Pts',(0.0928396337021713,-0.10383510521762,
0.110742281899551));
#39454=CARTESIAN_POINT('Ctrl Pts',(0.137550169005636,0.0219289054269618,
0.118694786014654));
#39455=CARTESIAN_POINT('Ctrl Pts',(0.0559501922162531,0.127555870431356,
0.126647290129757));
#39456=CARTESIAN_POINT('Ctrl Pts',(-0.0763838391282559,0.116105719252975,
0.134561265282744));
#39457=CARTESIAN_POINT('Ctrl Pts',(-0.117918750607874,0.0384749486295239,
0.139824405730697));
#39458=CARTESIAN_POINT('Ctrl Pts',(-0.117968412270431,-1.06668654225827E-5,
0.142436711473616));
#39459=CARTESIAN_POINT('Origin',(0.,0.,-0.0924367114736154));
#39460=CARTESIAN_POINT('',(-0.117919967015755,7.48285734863531E-5,0.0325632885263843));
#39461=CARTESIAN_POINT('',(-0.117605093279175,5.63740904734461E-5,0.042436711473616));
#39462=CARTESIAN_POINT('',(-0.117775,-8.88924268665971E-15,-0.0924367114736154));
#39463=CARTESIAN_POINT('Ctrl Pts',(-0.117919967015755,7.48285734863559E-5,
0.0325632885263843));
#39464=CARTESIAN_POINT('Ctrl Pts',(-0.117681732256532,-0.0350969523534404,
0.0349482868782861));
#39465=CARTESIAN_POINT('Ctrl Pts',(-0.0823020584651488,-0.1097611636214,
0.0399811708023271));
#39466=CARTESIAN_POINT('Ctrl Pts',(0.0446654385229893,-0.131869273048715,
0.0476619402985074));
#39467=CARTESIAN_POINT('Ctrl Pts',(0.135042047193827,-0.033912683303242,
0.0556055970149253));
#39468=CARTESIAN_POINT('Ctrl Pts',(0.101666114468308,0.0951356880412728,
0.0635492537313433));
#39469=CARTESIAN_POINT('Ctrl Pts',(-0.0248796065525388,0.136992916606216,
0.0714929104477611));
#39470=CARTESIAN_POINT('Ctrl Pts',(-0.107654697213721,0.0702257630245385,
0.0778309220461081));
#39471=CARTESIAN_POINT('Ctrl Pts',(-0.117693369175918,0.0155377418730691,
0.0815210480723159));
#39472=CARTESIAN_POINT('Ctrl Pts',(-0.117616583813332,6.4587952335533E-5,
0.0825632885263843));
#39473=CARTESIAN_POINT('Ctrl Pts',(-0.117605093279175,5.6374090473453E-5,
0.042436711473616));
#39474=CARTESIAN_POINT('Ctrl Pts',(-0.117506950346121,-0.0231366833782073,
0.0439985573086537));
#39475=CARTESIAN_POINT('Ctrl Pts',(-0.0996401976376468,-0.0858346907547986,
0.0482112378487256));
#39476=CARTESIAN_POINT('Ctrl Pts',(0.00241643506700816,-0.139265216174241,
0.0550747530938317));
#39477=CARTESIAN_POINT('Ctrl Pts',(0.118445458723555,-0.0732914200146354,
0.0630272572089346));
#39478=CARTESIAN_POINT('Ctrl Pts',(0.125708256673902,0.0599868231457294,
0.0709797613240373));
#39479=CARTESIAN_POINT('Ctrl Pts',(0.0175344664057042,0.138178956948752,
0.0789322654391402));
#39480=CARTESIAN_POINT('Ctrl Pts',(-0.0942361274410431,0.0943834610594897,
0.0860845821556665));
#39481=CARTESIAN_POINT('Ctrl Pts',(-0.117472740117216,0.0273268854223547,
0.0905860641671583));
#39482=CARTESIAN_POINT('Ctrl Pts',(-0.117696063073914,-0.000101172369946261,
0.092436711473616));
#39483=CARTESIAN_POINT('Origin',(0.,0.,0.55));
#39484=CARTESIAN_POINT('',(-0.143213254968838,-6.38556725402083E-7,0.507000235761732));
#39485=CARTESIAN_POINT('Ctrl Pts',(-0.0334019664626817,0.112939183906321,
0.532225));
#39486=CARTESIAN_POINT('Ctrl Pts',(-0.025060850432499,0.115799622360937,
0.531847620192936));
#39487=CARTESIAN_POINT('Ctrl Pts',(-0.0164290366846974,0.117635249741265,
0.531473612813392));
#39488=CARTESIAN_POINT('Ctrl Pts',(-0.00767275263448023,0.118510014194121,
0.531100586051555));
#39489=CARTESIAN_POINT('Ctrl Pts',(-0.00421690952474848,0.118855257529045,
0.530953363558858));
#39490=CARTESIAN_POINT('Ctrl Pts',(-0.000739669302851069,0.119050301419728,
0.530806218229583));
#39491=CARTESIAN_POINT('Ctrl Pts',(0.00274357664202706,0.119096927952431,
0.530659241408731));
#39492=CARTESIAN_POINT('Ctrl Pts',(0.00973382066470735,0.119190498962541,
0.5303642855372));
#39493=CARTESIAN_POINT('Ctrl Pts',(0.0167166427004772,0.118687723090435,
0.530071327820757));
#39494=CARTESIAN_POINT('Ctrl Pts',(0.023612882680227,0.11761343656186,0.529779224661465));
#39495=CARTESIAN_POINT('Ctrl Pts',(0.0274136336191392,0.117021360946144,
0.529618236737583));
#39496=CARTESIAN_POINT('Ctrl Pts',(0.0311881579134606,0.116255363574116,
0.529457508384123));
#39497=CARTESIAN_POINT('Ctrl Pts',(0.0349231679080101,0.115317271371855,
0.529296848155877));
#39498=CARTESIAN_POINT('Ctrl Pts',(0.037971953630239,0.114551532560831,
0.529165705639333));
#39499=CARTESIAN_POINT('Ctrl Pts',(0.0409939934565533,0.113670841591964,
0.529034622190513));
#39500=CARTESIAN_POINT('Ctrl Pts',(0.0439689729533011,0.112680856226694,
0.528904071147902));
#39501=CARTESIAN_POINT('Ctrl Pts',(0.0505577881110133,0.110488293021555,
0.528614934133899));
#39502=CARTESIAN_POINT('Ctrl Pts',(0.0569328249215936,0.107756906396238,
0.528327689901185));
#39503=CARTESIAN_POINT('Ctrl Pts',(0.0630179104963209,0.104502120084129,
0.528041256645784));
#39504=CARTESIAN_POINT('Ctrl Pts',(0.0668676595642169,0.102442968997859,
0.527860043720435));
#39505=CARTESIAN_POINT('Ctrl Pts',(0.0706013360983203,0.100173990889927,
0.527679155388847));
#39506=CARTESIAN_POINT('Ctrl Pts',(0.0741982818595768,0.0976957705995567,
0.527498317717128));
#39507=CARTESIAN_POINT('Ctrl Pts',(0.0762868294587642,0.0962568050489885,
0.527393315276118));
#39508=CARTESIAN_POINT('Ctrl Pts',(0.0783301222953497,0.0947465519651971,
0.527288283929736));
#39509=CARTESIAN_POINT('Ctrl Pts',(0.0803210903525092,0.0931669243552789,
0.527183314414725));
#39510=CARTESIAN_POINT('Ctrl Pts',(0.0873333522084643,0.0876034185040368,
0.526813607967904));
#39511=CARTESIAN_POINT('Ctrl Pts',(0.0936466399845286,0.0812254488323135,
0.526447434844115));
#39512=CARTESIAN_POINT('Ctrl Pts',(0.0992257444432458,0.0742158265894858,
0.526082561055055));
#39513=CARTESIAN_POINT('Ctrl Pts',(0.101943770530818,0.0708008813664647,
0.525904801974781));
#39514=CARTESIAN_POINT('Ctrl Pts',(0.104487132714136,0.0672353052679948,
0.525727351283807));
#39515=CARTESIAN_POINT('Ctrl Pts',(0.106849003984973,0.0635370592318222,
0.525549950667934));
#39516=CARTESIAN_POINT('Ctrl Pts',(0.108451822333258,0.0610273472604538,
0.525429562666425));
#39517=CARTESIAN_POINT('Ctrl Pts',(0.109972218146102,0.0584542637442968,
0.525309095710787));
#39518=CARTESIAN_POINT('Ctrl Pts',(0.111403508282751,0.0558304813946845,
0.525188806889777));
#39519=CARTESIAN_POINT('Ctrl Pts',(0.115946659550801,0.0475021629053002,
0.524806990306466));
#39520=CARTESIAN_POINT('Ctrl Pts',(0.119574294719482,0.0387078320373927,
0.524428851599571));
#39521=CARTESIAN_POINT('Ctrl Pts',(0.122229265704535,0.02963297991244,0.524051927142185));
#39522=CARTESIAN_POINT('Ctrl Pts',(0.123491040005696,0.0253201586942182,
0.523872793887439));
#39523=CARTESIAN_POINT('Ctrl Pts',(0.124532521003962,0.0209434889498052,
0.523693934885913));
#39524=CARTESIAN_POINT('Ctrl Pts',(0.125343829183128,0.0165211886089503,
0.523515085689393));
#39525=CARTESIAN_POINT('Ctrl Pts',(0.126073723283802,0.0125426623065107,
0.523354183856031));
#39526=CARTESIAN_POINT('Ctrl Pts',(0.126617185118597,0.00852274589339418,
0.523193115530006));
#39527=CARTESIAN_POINT('Ctrl Pts',(0.126964066890117,0.00450317609134152,
0.523032822082874));
#39528=CARTESIAN_POINT('Ctrl Pts',(0.127610380106321,-0.00298612228009172,
0.522734161899901));
#39529=CARTESIAN_POINT('Ctrl Pts',(0.127580071374667,-0.0104910608890547,
0.522437493943663));
#39530=CARTESIAN_POINT('Ctrl Pts',(0.126833825603371,-0.0179253657039838,
0.52214162882945));
#39531=CARTESIAN_POINT('Ctrl Pts',(0.126370997360361,-0.0225361874571381,
0.521958130662699));
#39532=CARTESIAN_POINT('Ctrl Pts',(0.125632379838884,-0.0271199619342287,
0.521774941316387));
#39533=CARTESIAN_POINT('Ctrl Pts',(0.124632255285918,-0.0316602427367966,
0.52159177704026));
#39534=CARTESIAN_POINT('Ctrl Pts',(0.123677051866189,-0.0359965943804856,
0.521416839686298));
#39535=CARTESIAN_POINT('Ctrl Pts',(0.122480780227546,-0.0402989646849493,
0.521241685776095));
#39536=CARTESIAN_POINT('Ctrl Pts',(0.121065837229724,-0.044520244829744,
0.521067408183846));
#39537=CARTESIAN_POINT('Ctrl Pts',(0.118338362465597,-0.0526572758514579,
0.520731466922931));
#39538=CARTESIAN_POINT('Ctrl Pts',(0.114798640009948,-0.0605127756442529,
0.520398022841861));
#39539=CARTESIAN_POINT('Ctrl Pts',(0.11054080941355,-0.0679858568570343,
0.520065383890604));
#39540=CARTESIAN_POINT('Ctrl Pts',(0.108372779925159,-0.0717910482735648,
0.5198960086562));
#39541=CARTESIAN_POINT('Ctrl Pts',(0.10601800718922,-0.0754969965361626,
0.51972684216845));
#39542=CARTESIAN_POINT('Ctrl Pts',(0.103485875290119,-0.0790891197455118,
0.519557661047695));
#39543=CARTESIAN_POINT('Ctrl Pts',(0.101239265068231,-0.0822761972920135,
0.519407556688845));
#39544=CARTESIAN_POINT('Ctrl Pts',(0.0988505693656959,-0.0853758696950735,
0.519257316754896));
#39545=CARTESIAN_POINT('Ctrl Pts',(0.0963426843438634,-0.0883583266502687,
0.51910776182463));
#39546=CARTESIAN_POINT('Ctrl Pts',(0.0906830843157466,-0.0950889037383469,
0.518770257880003));
#39547=CARTESIAN_POINT('Ctrl Pts',(0.084404823468622,-0.101245530098652,
0.518435260730044));
#39548=CARTESIAN_POINT('Ctrl Pts',(0.077590384105458,-0.106717161154373,
0.51810105566737));
#39549=CARTESIAN_POINT('Ctrl Pts',(0.072812396824573,-0.110553629893275,
0.517866725672845));
#39550=CARTESIAN_POINT('Ctrl Pts',(0.0677701261881638,-0.114053116790221,
0.517632785084427));
#39551=CARTESIAN_POINT('Ctrl Pts',(0.0624852082906241,-0.117169678449436,
0.517398642838002));
#39552=CARTESIAN_POINT('Ctrl Pts',(0.060232694538615,-0.11849800523378,
0.517298847790998));
#39553=CARTESIAN_POINT('Ctrl Pts',(0.0579421351333471,-0.119753052219492,
0.517199285984453));
#39554=CARTESIAN_POINT('Ctrl Pts',(0.0556164103289471,-0.120931647626768,
0.517099943244175));
#39555=CARTESIAN_POINT('Ctrl Pts',(0.0470766353824801,-0.125259304756293,
0.516735168941155));
#39556=CARTESIAN_POINT('Ctrl Pts',(0.0380619111816488,-0.128561628767388,
0.516373216300106));
#39557=CARTESIAN_POINT('Ctrl Pts',(0.0287540615399164,-0.13087769180711,
0.516011917283344));
#39558=CARTESIAN_POINT('Ctrl Pts',(0.0244834739512418,-0.131940337901829,
0.515846147620515));
#39559=CARTESIAN_POINT('Ctrl Pts',(0.0201508023558736,-0.132794720803219,
0.515680515553343));
#39560=CARTESIAN_POINT('Ctrl Pts',(0.0157724288157125,-0.133441328903782,
0.515514811679433));
#39561=CARTESIAN_POINT('Ctrl Pts',(0.0127414878228209,-0.13388894512025,
0.515400102721983));
#39562=CARTESIAN_POINT('Ctrl Pts',(0.0096905970655013,-0.134236406792975,
0.515285434752076));
#39563=CARTESIAN_POINT('Ctrl Pts',(0.00663678161128016,-0.134483505205774,
0.515171166690044));
#39564=CARTESIAN_POINT('Ctrl Pts',(-0.00335208404858516,-0.135291750788136,
0.514797402021565));
#39565=CARTESIAN_POINT('Ctrl Pts',(-0.0134050142894213,-0.135035519709951,
0.514426646108251));
#39566=CARTESIAN_POINT('Ctrl Pts',(-0.0233297246571887,-0.13373576937046,
0.514056571073779));
#39567=CARTESIAN_POINT('Ctrl Pts',(-0.0275876193693317,-0.133178151073044,
0.5138978016514));
#39568=CARTESIAN_POINT('Ctrl Pts',(-0.0318220223293205,-0.132427814053447,
0.513739157550061));
#39569=CARTESIAN_POINT('Ctrl Pts',(-0.0360175989408762,-0.131483472271743,
0.513580454950452));
#39570=CARTESIAN_POINT('Ctrl Pts',(-0.0391091145169674,-0.130787632915777,
0.513463514752696));
#39571=CARTESIAN_POINT('Ctrl Pts',(-0.0421792587373029,-0.12998615137042,
0.513346550232001));
#39572=CARTESIAN_POINT('Ctrl Pts',(-0.0452082926810733,-0.129082949079949,
0.513230012664731));
#39573=CARTESIAN_POINT('Ctrl Pts',(-0.0547989520179786,-0.126223190608758,
0.512861026338271));
#39574=CARTESIAN_POINT('Ctrl Pts',(-0.0640135938008781,-0.122340292920341,
0.512494993993967));
#39575=CARTESIAN_POINT('Ctrl Pts',(-0.0726621826878073,-0.117434240919462,
0.512129678956248));
#39576=CARTESIAN_POINT('Ctrl Pts',(-0.0732258670681981,-0.11711448183293,
0.512105869016456));
#39577=CARTESIAN_POINT('Ctrl Pts',(-0.073787141143001,-0.116790358750658,
0.512082062123761));
#39578=CARTESIAN_POINT('Ctrl Pts',(-0.0743459493499517,-0.11646186427858,
0.5120582576589));
#39579=CARTESIAN_POINT('Ctrl Pts',(-0.0780940452153038,-0.11425855237787,
0.511898593904482));
#39580=CARTESIAN_POINT('Ctrl Pts',(-0.0817313018976771,-0.111858709629848,
0.511739039373249));
#39581=CARTESIAN_POINT('Ctrl Pts',(-0.085250803842968,-0.109275770384611,
0.511579407204066));
#39582=CARTESIAN_POINT('Ctrl Pts',(-0.0875213278289363,-0.107609447819153,
0.511476424260826));
#39583=CARTESIAN_POINT('Ctrl Pts',(-0.0897413530091093,-0.105867722400153,
0.511373470200391));
#39584=CARTESIAN_POINT('Ctrl Pts',(-0.0919020268850941,-0.104060687103246,
0.511270839257698));
#39585=CARTESIAN_POINT('Ctrl Pts',(-0.0994865656445924,-0.0977175136139456,
0.510910577410027));
#39586=CARTESIAN_POINT('Ctrl Pts',(-0.106368098520952,-0.0905540945926997,
0.510553119515254));
#39587=CARTESIAN_POINT('Ctrl Pts',(-0.112476669881714,-0.082740585635558,
0.510196385012091));
#39588=CARTESIAN_POINT('Ctrl Pts',(-0.115701946031867,-0.0786151162581588,
0.510008032086826));
#39589=CARTESIAN_POINT('Ctrl Pts',(-0.118711292938496,-0.0743076837297934,
0.509819880825374));
#39590=CARTESIAN_POINT('Ctrl Pts',(-0.121490605137305,-0.0698396458594739,
0.509631624987483));
#39591=CARTESIAN_POINT('Ctrl Pts',(-0.123158603264919,-0.0671581627195108,
0.509518643658775));
#39592=CARTESIAN_POINT('Ctrl Pts',(-0.124742701375389,-0.0644198867277164,
0.509405676189658));
#39593=CARTESIAN_POINT('Ctrl Pts',(-0.126234357059848,-0.06164059243669,
0.509293097144302));
#39594=CARTESIAN_POINT('Ctrl Pts',(-0.131306921574689,-0.0521892493795411,
0.508910257809098));
#39595=CARTESIAN_POINT('Ctrl Pts',(-0.135335100093566,-0.0422336175385342,
0.508530533331389));
#39596=CARTESIAN_POINT('Ctrl Pts',(-0.138212265982587,-0.0319628814891436,
0.508151426353207));
#39597=CARTESIAN_POINT('Ctrl Pts',(-0.139343321582236,-0.0279253063303673,
0.508002393907016));
#39598=CARTESIAN_POINT('Ctrl Pts',(-0.140295939750969,-0.0238387054236251,
0.507853456888584));
#39599=CARTESIAN_POINT('Ctrl Pts',(-0.14106118303298,-0.0197137190414539,
0.507704463579619));
#39600=CARTESIAN_POINT('Ctrl Pts',(-0.141663078970186,-0.0164692442413196,
0.507587274093027));
#39601=CARTESIAN_POINT('Ctrl Pts',(-0.142148737315268,-0.0132004963364534,
0.507470032942495));
#39602=CARTESIAN_POINT('Ctrl Pts',(-0.14251240365623,-0.00992818124989041,
0.507353216880015));
#39603=CARTESIAN_POINT('Ctrl Pts',(-0.14286252481498,-0.00677774740200931,
0.507240751769694));
#39604=CARTESIAN_POINT('Ctrl Pts',(-0.143100295244155,-0.00362062020727709,
0.507128557913111));
#39605=CARTESIAN_POINT('Ctrl Pts',(-0.143222931917338,-0.0004616047295162,
0.507016572073626));
#39606=CARTESIAN_POINT('Ctrl Pts',(-0.143228895796354,-0.000307980323141247,
0.507011126149655));
#39607=CARTESIAN_POINT('Ctrl Pts',(-0.143234587305958,-0.000154351422170947,
0.50700568071763));
#39608=CARTESIAN_POINT('Ctrl Pts',(-0.143240006909252,-7.18572550341278E-7,
0.507000235770275));
#39609=CARTESIAN_POINT('',(-0.00156805256656782,0.146109107730171,0.50365));
#39610=CARTESIAN_POINT('Ctrl Pts',(-0.0015703316452181,0.146071601053478,
0.50365));
#39611=CARTESIAN_POINT('Ctrl Pts',(-0.0117120407853717,0.144648246558049,
0.504950624278524));
#39612=CARTESIAN_POINT('Ctrl Pts',(-0.0216505365241647,0.142222557694311,
0.506260995613922));
#39613=CARTESIAN_POINT('Ctrl Pts',(-0.0312063389538959,0.13880538472021,
0.507590209176103));
#39614=CARTESIAN_POINT('Ctrl Pts',(-0.0379631701734481,0.136389129130603,
0.508530085419929));
#39615=CARTESIAN_POINT('Ctrl Pts',(-0.0445284394867549,0.133476109724793,
0.50947938238263));
#39616=CARTESIAN_POINT('Ctrl Pts',(-0.050827361354341,0.13005807034167,
0.510441315490383));
#39617=CARTESIAN_POINT('Ctrl Pts',(-0.0535603409840707,0.12857504956382,
0.510858679547901));
#39618=CARTESIAN_POINT('Ctrl Pts',(-0.056235007151428,0.127001156165417,
0.511277203939051));
#39619=CARTESIAN_POINT('Ctrl Pts',(-0.0588447172056459,0.125337452214503,
0.511696981696819));
#39620=CARTESIAN_POINT('Ctrl Pts',(-0.0624191770014244,0.123058715204999,
0.512271941629964));
#39621=CARTESIAN_POINT('Ctrl Pts',(-0.0658727208815536,0.120611069028702,
0.512849385708712));
#39622=CARTESIAN_POINT('Ctrl Pts',(-0.0691906694557284,0.117994047416377,
0.513430106410014));
#39623=CARTESIAN_POINT('Ctrl Pts',(-0.0733832729377804,0.114687144467415,
0.51416391273038));
#39624=CARTESIAN_POINT('Ctrl Pts',(-0.0773595119772722,0.111109779201256,
0.514902950893669));
#39625=CARTESIAN_POINT('Ctrl Pts',(-0.0811052238678245,0.107288843574283,
0.515648819828442));
#39626=CARTESIAN_POINT('Ctrl Pts',(-0.0841017207582698,0.104232169153142,
0.516245500515327));
#39627=CARTESIAN_POINT('Ctrl Pts',(-0.0869506135922833,0.101019546539762,
0.516846552684068));
#39628=CARTESIAN_POINT('Ctrl Pts',(-0.0896425492995218,0.097664267789728,
0.517452794926569));
#39629=CARTESIAN_POINT('Ctrl Pts',(-0.0913307146861822,0.0955601070428074,
0.517832981261246));
#39630=CARTESIAN_POINT('Ctrl Pts',(-0.0929559105919431,0.0934010507133458,
0.518214974249558));
#39631=CARTESIAN_POINT('Ctrl Pts',(-0.094511034598742,0.0911980939617143,
0.518597709131816));
#39632=CARTESIAN_POINT('Ctrl Pts',(-0.0989061554610084,0.0849720559509604,
0.519679401690337));
#39633=CARTESIAN_POINT('Ctrl Pts',(-0.102756278369653,0.0783797189661076,
0.520769927597638));
#39634=CARTESIAN_POINT('Ctrl Pts',(-0.106019480011838,0.0715022869017531,
0.521874709646989));
#39635=CARTESIAN_POINT('Ctrl Pts',(-0.10810684462629,0.0671030159085511,
0.522581403014228));
#39636=CARTESIAN_POINT('Ctrl Pts',(-0.109953633570546,0.0625869322502571,
0.523293929634644));
#39637=CARTESIAN_POINT('Ctrl Pts',(-0.111544021459737,0.0579753350677128,
0.524013708847662));
#39638=CARTESIAN_POINT('Ctrl Pts',(-0.11291963712523,0.0539865060717378,
0.524636286250227));
#39639=CARTESIAN_POINT('Ctrl Pts',(-0.114104149138597,0.0499208096400247,
0.525265113718246));
#39640=CARTESIAN_POINT('Ctrl Pts',(-0.115079157041328,0.0458232444145113,
0.525896440126774));
#39641=CARTESIAN_POINT('Ctrl Pts',(-0.117097797518837,0.0373397121269415,
0.527203528037759));
#39642=CARTESIAN_POINT('Ctrl Pts',(-0.118231089846825,0.0286982113614575,
0.528524583654289));
#39643=CARTESIAN_POINT('Ctrl Pts',(-0.118391363114938,0.0200276346563605,
0.529869408057975));
#39644=CARTESIAN_POINT('Ctrl Pts',(-0.118483921504357,0.0150203453896601,
0.530646048993314));
#39645=CARTESIAN_POINT('Ctrl Pts',(-0.118251089036742,0.0100034984621487,
0.531430617066573));
#39646=CARTESIAN_POINT('Ctrl Pts',(-0.117668597464311,0.00500517689817885,
0.532225));
#39647=CARTESIAN_POINT('',(-0.115076068242798,0.0902060425677366,0.50365));
#39648=CARTESIAN_POINT('Origin',(0.,0.,0.50365));
#39649=CARTESIAN_POINT('Ctrl Pts',(-0.143240006909252,-7.18572550341278E-7,
0.507000235770275));
#39650=CARTESIAN_POINT('Ctrl Pts',(-0.143520908694302,0.00796217822295569,
0.506718020385041));
#39651=CARTESIAN_POINT('Ctrl Pts',(-0.14307308860376,0.0159355469497794,
0.506437106818574));
#39652=CARTESIAN_POINT('Ctrl Pts',(-0.141950240996583,0.0238446282639654,
0.506156482679269));
#39653=CARTESIAN_POINT('Ctrl Pts',(-0.141327877173321,0.0282284164590215,
0.506000940367809));
#39654=CARTESIAN_POINT('Ctrl Pts',(-0.140497759623186,0.0325924948231262,
0.505845486973662));
#39655=CARTESIAN_POINT('Ctrl Pts',(-0.139466483050223,0.0369239027928834,
0.505689950104037));
#39656=CARTESIAN_POINT('Ctrl Pts',(-0.138800760016326,0.0397199694642927,
0.50558954592591));
#39657=CARTESIAN_POINT('Ctrl Pts',(-0.138051361267828,0.0425008441913541,
0.50548916176982));
#39658=CARTESIAN_POINT('Ctrl Pts',(-0.137223245651255,0.0452539885083259,
0.505389082377033));
#39659=CARTESIAN_POINT('Ctrl Pts',(-0.134183880382411,0.0553586297560613,
0.505021769136614));
#39660=CARTESIAN_POINT('Ctrl Pts',(-0.130080477516678,0.06512485891418,
0.504657328869907));
#39661=CARTESIAN_POINT('Ctrl Pts',(-0.125019236367424,0.0743847486871139,
0.504293559587933));
#39662=CARTESIAN_POINT('Ctrl Pts',(-0.122033398952289,0.0798475441810871,
0.504078956904408));
#39663=CARTESIAN_POINT('Ctrl Pts',(-0.118713161823888,0.0851340339476938,
0.503864587744543));
#39664=CARTESIAN_POINT('Ctrl Pts',(-0.115072616245007,0.0902061753896176,
0.50365));
#39665=CARTESIAN_POINT('',(-0.05,-6.12323399573676E-18,0.6));
#39666=CARTESIAN_POINT('',(-0.1,-1.22464679914735E-17,0.55));
#39667=CARTESIAN_POINT('Origin',(0.,0.,0.6));
#39668=CARTESIAN_POINT('Ctrl Pts',(0.0850780204044556,-0.119080027477571,
-0.0164977839420937));
#39669=CARTESIAN_POINT('Ctrl Pts',(0.124701079614845,-0.0907709019978731,
-0.0138498983699544));
#39670=CARTESIAN_POINT('Ctrl Pts',(0.172780327456066,0.00801716155080004,
-0.00855412722567576));
#39671=CARTESIAN_POINT('Ctrl Pts',(0.0867037234097596,0.149857524855506,
-0.000610470509257829));
#39672=CARTESIAN_POINT('Ctrl Pts',(-0.0789008477636886,0.153920736728128,
0.00733318620716008));
#39673=CARTESIAN_POINT('Ctrl Pts',(-0.172161895422237,0.0171520622219753,
0.015276842923578));
#39674=CARTESIAN_POINT('Ctrl Pts',(-0.107670523249975,-0.135451540092597,
0.0232204996399959));
#39675=CARTESIAN_POINT('Ctrl Pts',(0.0555023301026467,-0.163863876974566,
0.0311641563564139));
#39676=CARTESIAN_POINT('Ctrl Pts',(0.167806441153186,-0.042140702198512,
0.0391078130728317));
#39677=CARTESIAN_POINT('Ctrl Pts',(0.126332717914983,0.118217855613161,
0.0470514697892497));
#39678=CARTESIAN_POINT('Ctrl Pts',(-0.0309159874248675,0.170230637616809,
0.0549951265056676));
#39679=CARTESIAN_POINT('Ctrl Pts',(-0.159831956410111,0.066245824895792,
0.0629387832220855));
#39680=CARTESIAN_POINT('Ctrl Pts',(-0.14227559413168,-0.0984502643440673,
0.0708824399385034));
#39681=CARTESIAN_POINT('Ctrl Pts',(0.00566478568548768,-0.172923543714354,
0.0788260966549214));
#39682=CARTESIAN_POINT('Ctrl Pts',(0.148413742858461,-0.0889274008243077,
0.0867697533713393));
#39683=CARTESIAN_POINT('Ctrl Pts',(0.155153858530075,0.0765636983283585,
0.0947134100877573));
#39684=CARTESIAN_POINT('Ctrl Pts',(0.0197082819896427,0.171890320651054,
0.102657066804175));
#39685=CARTESIAN_POINT('Ctrl Pts',(-0.133798285716779,0.109693800981729,
0.110600723520593));
#39686=CARTESIAN_POINT('Ctrl Pts',(-0.164689815771182,-0.0530280538225922,
0.118544380237011));
#39687=CARTESIAN_POINT('Ctrl Pts',(-0.044656766037051,-0.167154062007556,
0.126488036953429));
#39688=CARTESIAN_POINT('Ctrl Pts',(0.11630050845274,-0.128097231996654,
0.134431693669847));
#39689=CARTESIAN_POINT('Ctrl Pts',(0.170678001253376,0.0283501086412318,
0.142375350386265));
#39690=CARTESIAN_POINT('Ctrl Pts',(0.0686432422541576,0.158816918899349,
0.150319007102683));
#39691=CARTESIAN_POINT('Ctrl Pts',(-0.0962973622855325,0.143741179688805,
0.1582626638191));
#39692=CARTESIAN_POINT('Ctrl Pts',(-0.172989410659926,-0.00306144592864502,
0.166206320535519));
#39693=CARTESIAN_POINT('Ctrl Pts',(-0.0911509925455794,-0.147058509343496,
0.174149977251936));
#39694=CARTESIAN_POINT('Ctrl Pts',(0.0742197602705133,-0.1562886299111,
0.182093633968354));
#39695=CARTESIAN_POINT('Ctrl Pts',(0.171574250349044,-0.0222931661803689,
0.190037290684772));
#39696=CARTESIAN_POINT('Ctrl Pts',(0.111695151232628,0.132132137756553,
0.19798094740119));
#39697=CARTESIAN_POINT('Ctrl Pts',(-0.0505433024217535,0.165469281811646,
0.205924604117608));
#39698=CARTESIAN_POINT('Ctrl Pts',(-0.16646300584434,0.0471675346608595,
0.213868260834026));
#39699=CARTESIAN_POINT('Ctrl Pts',(-0.129833152315396,-0.11435935117077,
0.221811917550444));
#39700=CARTESIAN_POINT('Ctrl Pts',(0.0257780314041745,-0.171085363892111,
0.229755574266861));
#39701=CARTESIAN_POINT('Ctrl Pts',(0.157765784501968,-0.0710258113735757,
0.23769923098328));
#39702=CARTESIAN_POINT('Ctrl Pts',(0.145174263631334,0.0941230142947892,
0.245642887699697));
#39703=CARTESIAN_POINT('Ctrl Pts',(-0.000457445268631668,0.173015893445265,
0.253586544416116));
#39704=CARTESIAN_POINT('Ctrl Pts',(-0.145669943468849,0.0933540369270586,
0.261530201132533));
#39705=CARTESIAN_POINT('Ctrl Pts',(-0.15738800412666,-0.0718590620464598,
0.269473857848952));
#39706=CARTESIAN_POINT('Ctrl Pts',(-0.0248729952365478,-0.171219282641631,
0.277417514565369));
#39707=CARTESIAN_POINT('Ctrl Pts',(0.130436053586269,-0.11367121256306,
0.285361171281788));
#39708=CARTESIAN_POINT('Ctrl Pts',(0.166211263149388,0.0480471086044073,
0.293304827998205));
#39709=CARTESIAN_POINT('Ctrl Pts',(0.0496676170739063,0.16573423439711,
0.301248484714623));
#39710=CARTESIAN_POINT('Ctrl Pts',(-0.112392286114514,0.131539661939415,
0.309192141431041));
#39711=CARTESIAN_POINT('Ctrl Pts',(-0.171453968444308,-0.0232001154910803,
0.317135798147459));
#39712=CARTESIAN_POINT('Ctrl Pts',(-0.0733922898759408,-0.156678908596981,
0.325079454863877));
#39713=CARTESIAN_POINT('Ctrl Pts',(0.0919273431499614,-0.146574459688691,
0.333023111580294));
#39714=CARTESIAN_POINT('Ctrl Pts',(0.173003180832518,-0.00214665863879225,
0.340966768296713));
#39715=CARTESIAN_POINT('Ctrl Pts',(0.0955359320753977,0.14424837648421,
0.34891042501313));
#39716=CARTESIAN_POINT('Ctrl Pts',(-0.0694820837435447,0.158451723911329,
0.356854081729549));
#39717=CARTESIAN_POINT('Ctrl Pts',(-0.170825527907542,0.0274471879557805,
0.364797738445966));
#39718=CARTESIAN_POINT('Ctrl Pts',(-0.115621519313607,-0.128710417100276,
0.372741395162384));
#39719=CARTESIAN_POINT('Ctrl Pts',(0.0455400241630207,-0.16691559576681,
0.380685051878803));
#39720=CARTESIAN_POINT('Ctrl Pts',(0.164967928025121,-0.0521564373559641,
0.38862870859522));
#39721=CARTESIAN_POINT('Ctrl Pts',(0.133216350942249,0.110399739828213,
0.396572365311638));
#39722=CARTESIAN_POINT('Ctrl Pts',(-0.0206169035662114,0.171783768167507,
0.404516022028056));
#39723=CARTESIAN_POINT('Ctrl Pts',(-0.155556614414135,0.0757420715232724,
0.412459678744474));
#39724=CARTESIAN_POINT('Ctrl Pts',(-0.14794130513946,-0.0897107128565239,
0.420403335460892));
#39725=CARTESIAN_POINT('Ctrl Pts',(-0.00475055195827078,-0.17295152931105,
0.42834699217731));
#39726=CARTESIAN_POINT('Ctrl Pts',(0.142794654932494,-0.0976957016900834,
0.436290648893728));
#39727=CARTESIAN_POINT('Ctrl Pts',(0.159478551636871,0.0670884478109748,
0.444234305610146));
#39728=CARTESIAN_POINT('Ctrl Pts',(0.0300170551768464,0.170394816235914,
0.452177962326563));
#39729=CARTESIAN_POINT('Ctrl Pts',(-0.126959218666436,0.117542321186412,
0.460121619042982));
#39730=CARTESIAN_POINT('Ctrl Pts',(-0.167575279308382,-0.043016329325927,
0.468065275759399));
#39731=CARTESIAN_POINT('Ctrl Pts',(-0.054646434915416,-0.164176211557628,
0.476008932475817));
#39732=CARTESIAN_POINT('Ctrl Pts',(0.108406899182729,-0.134840111552273,
0.483952589192236));
#39733=CARTESIAN_POINT('Ctrl Pts',(0.172027477869207,0.0179856562492908,
0.491896245908652));
#39734=CARTESIAN_POINT('Ctrl Pts',(0.0781660714022324,0.154482616143293,
0.499839902625072));
#39735=CARTESIAN_POINT('Ctrl Pts',(-0.0876620486424683,0.149106276403653,
0.507783559341488));
#39736=CARTESIAN_POINT('Ctrl Pts',(-0.144148268866352,0.0548725112369506,
0.513079330485768));
#39737=CARTESIAN_POINT('Ctrl Pts',(-0.146217781693075,0.00621955117001058,
0.515727216057907));
#39738=CARTESIAN_POINT('Ctrl Pts',(0.0795408277542857,-0.111329858282327,
-0.0109985226280625));
#39739=CARTESIAN_POINT('Ctrl Pts',(0.116585071529219,-0.0848631955302966,
-0.00835063705592319));
#39740=CARTESIAN_POINT('Ctrl Pts',(0.161535143861813,0.00749537498591264,
-0.00305486591164458));
#39741=CARTESIAN_POINT('Ctrl Pts',(0.0810607239872927,0.140104242147965,
0.00488879080477336));
#39742=CARTESIAN_POINT('Ctrl Pts',(-0.0737656883858339,0.143903005144011,
0.0128324475211912));
#39743=CARTESIAN_POINT('Ctrl Pts',(-0.160956961675077,0.0160357424907528,
0.0207761042376092));
#39744=CARTESIAN_POINT('Ctrl Pts',(-0.100662926844399,-0.12663585222528,
0.028719760954027));
#39745=CARTESIAN_POINT('Ctrl Pts',(0.0518900329094276,-0.153199008999282,
0.0366634176704451));
#39746=CARTESIAN_POINT('Ctrl Pts',(0.156884976500066,-0.039398029233422,
0.0446070743868629));
#39747=CARTESIAN_POINT('Ctrl Pts',(0.118110516766091,0.110523799755865,
0.052550731103281));
#39748=CARTESIAN_POINT('Ctrl Pts',(-0.0289038604674246,0.159151397279945,
0.0604943878196987));
#39749=CARTESIAN_POINT('Ctrl Pts',(-0.149429500757181,0.0619343012734311,
0.0684380445361168));
#39750=CARTESIAN_POINT('Ctrl Pts',(-0.133015771554951,-0.0920427565348621,
0.0763817012525346));
#39751=CARTESIAN_POINT('Ctrl Pts',(0.00529610045382266,-0.161669039075616,
0.0843253579689526));
#39752=CARTESIAN_POINT('Ctrl Pts',(0.138754426830263,-0.0831396762404221,
0.0922690146853704));
#39753=CARTESIAN_POINT('Ctrl Pts',(0.145055870812282,0.0715806492912723,
0.100212671401788));
#39754=CARTESIAN_POINT('Ctrl Pts',(0.0184255940091067,0.160703061995767,
0.108156328118206));
#39755=CARTESIAN_POINT('Ctrl Pts',(-0.125090197766985,0.102554522168261,
0.116099984834624));
#39756=CARTESIAN_POINT('Ctrl Pts',(-0.153971192640191,-0.0495767916930391,
0.124043641551042));
#39757=CARTESIAN_POINT('Ctrl Pts',(-0.0417503383192307,-0.156275056605288,
0.13198729826746));
#39758=CARTESIAN_POINT('Ctrl Pts',(0.108731240649445,-0.119760189736536,
0.139930954983878));
#39759=CARTESIAN_POINT('Ctrl Pts',(0.159569644834255,0.0265049785776333,
0.147874611700296));
#39760=CARTESIAN_POINT('Ctrl Pts',(0.0641756858313974,0.148480525646761,
0.155818268416713));
#39761=CARTESIAN_POINT('Ctrl Pts',(-0.0900299733154633,0.134385971376294,
0.163761925133132));
#39762=CARTESIAN_POINT('Ctrl Pts',(-0.161730619156435,-0.00286219568969563,
0.171705581849549));
#39763=CARTESIAN_POINT('Ctrl Pts',(-0.0852185483775114,-0.137487396931492,
0.179649238565968));
#39764=CARTESIAN_POINT('Ctrl Pts',(0.0693892634028907,-0.14611678706926,
0.187592895282385));
#39765=CARTESIAN_POINT('Ctrl Pts',(0.160407562719562,-0.0208422443637096,
0.195536551998804));
#39766=CARTESIAN_POINT('Ctrl Pts',(0.104425617132929,0.123532488886508,
0.203480208715221));
#39767=CARTESIAN_POINT('Ctrl Pts',(-0.0472537571155211,0.154699928144028,
0.211423865431639));
#39768=CARTESIAN_POINT('Ctrl Pts',(-0.155628976936467,0.0440976968224941,
0.219367522148057));
#39769=CARTESIAN_POINT('Ctrl Pts',(-0.121383129932039,-0.106916421072365,
0.227311178864475));
#39770=CARTESIAN_POINT('Ctrl Pts',(0.0241003016527248,-0.159950494803813,
0.235254835580893));
#39771=CARTESIAN_POINT('Ctrl Pts',(0.147497802968786,-0.0664031885287967,
0.243198492297311));
#39772=CARTESIAN_POINT('Ctrl Pts',(0.135725784908488,0.0879971399445481,
0.251142149013729));
#39773=CARTESIAN_POINT('Ctrl Pts',(-0.000427673036423806,0.161755378344027,
0.259085805730147));
#39774=CARTESIAN_POINT('Ctrl Pts',(-0.136189204066452,0.0872782104717779,
0.267029462446565));
#39775=CARTESIAN_POINT('Ctrl Pts',(-0.147144609939394,-0.067182208161988,
0.274973119162982));
#39776=CARTESIAN_POINT('Ctrl Pts',(-0.0232541685906426,-0.160075697625154,
0.282916775879401));
#39777=CARTESIAN_POINT('Ctrl Pts',(0.12194679215539,-0.106273069073731,
0.290860432595819));
#39778=CARTESIAN_POINT('Ctrl Pts',(0.155393618588418,0.0449200248363383,
0.298804089312236));
#39779=CARTESIAN_POINT('Ctrl Pts',(0.0464350646131678,0.154947636633991,
0.306747746028654));
#39780=CARTESIAN_POINT('Ctrl Pts',(-0.105077379894898,0.122978573589753,
0.314691402745072));
#39781=CARTESIAN_POINT('Ctrl Pts',(-0.160295109206645,-0.021690166054439,
0.32263505946149));
#39782=CARTESIAN_POINT('Ctrl Pts',(-0.0686156478460915,-0.146481664972887,
0.330578716177908));
#39783=CARTESIAN_POINT('Ctrl Pts',(0.0859443712093853,-0.137034851020875,
0.338522372894326));
#39784=CARTESIAN_POINT('Ctrl Pts',(0.161743493115198,-0.00200694614453471,
0.346466029610744));
#39785=CARTESIAN_POINT('Ctrl Pts',(0.0893180998033222,0.134860157925877,
0.354409686327162));
#39786=CARTESIAN_POINT('Ctrl Pts',(-0.0649599324100484,0.148139098901043,
0.36235334304358));
#39787=CARTESIAN_POINT('Ctrl Pts',(-0.159707569907411,0.0256608233143121,
0.370296999759998));
#39788=CARTESIAN_POINT('Ctrl Pts',(-0.108096442638088,-0.120333466482715,
0.378240656476415));
#39789=CARTESIAN_POINT('Ctrl Pts',(0.0425761107352605,-0.156052110630637,
0.386184313192834));
#39790=CARTESIAN_POINT('Ctrl Pts',(0.154231204318669,-0.0487619032540464,
0.394127969909251));
#39791=CARTESIAN_POINT('Ctrl Pts',(0.124546137462748,0.103214515900207,
0.402071626625669));
#39792=CARTESIAN_POINT('Ctrl Pts',(-0.0192750791284384,0.160603444342461,
0.410015283342087));
#39793=CARTESIAN_POINT('Ctrl Pts',(-0.145432413851821,0.0708124970015145,
0.417958940058505));
#39794=CARTESIAN_POINT('Ctrl Pts',(-0.138312737107664,-0.0838720074246256,
0.425902596774923));
#39795=CARTESIAN_POINT('Ctrl Pts',(-0.00444136844339109,-0.161695203266036,
0.433846253491342));
#39796=CARTESIAN_POINT('Ctrl Pts',(0.133501049956532,-0.0913373036128839,
0.441789910207758));
#39797=CARTESIAN_POINT('Ctrl Pts',(0.1490990968754,0.0627220831686826,0.449733566924177));
#39798=CARTESIAN_POINT('Ctrl Pts',(0.0280634340592545,0.159304890546491,
0.457677223640594));
#39799=CARTESIAN_POINT('Ctrl Pts',(-0.118696242528426,0.109892231611416,
0.465620880357014));
#39800=CARTESIAN_POINT('Ctrl Pts',(-0.156668859524218,-0.0402166673045443,
0.47356453707343));
#39801=CARTESIAN_POINT('Ctrl Pts',(-0.0510898425507461,-0.153491015690964,
0.481508193789849));
#39802=CARTESIAN_POINT('Ctrl Pts',(0.101351376704318,-0.126064217718754,
0.489451850506266));
#39803=CARTESIAN_POINT('Ctrl Pts',(0.160831292514208,0.0168150831315976,
0.497395507222684));
#39804=CARTESIAN_POINT('Ctrl Pts',(0.0730787339911879,0.144428315365945,
0.505339163939102));
#39805=CARTESIAN_POINT('Ctrl Pts',(-0.0819566778647476,0.13940188772757,
0.51328282065552));
#39806=CARTESIAN_POINT('Ctrl Pts',(-0.134766565682532,0.0513012049880128,
0.518578591799799));
#39807=CARTESIAN_POINT('Ctrl Pts',(-0.136701386950153,0.005814759746065,
0.521226477371938));
#39808=CARTESIAN_POINT('Ctrl Pts',(0.0740036351041157,-0.103579689087084,
-0.00549926131403131));
#39809=CARTESIAN_POINT('Ctrl Pts',(0.108469063443593,-0.0789554890627202,
-0.00285137574189201));
#39810=CARTESIAN_POINT('Ctrl Pts',(0.150289960267559,0.00697358842102527,
0.00244439540238661));
#39811=CARTESIAN_POINT('Ctrl Pts',(0.0754177245648256,0.130350959440424,
0.0103880521188046));
#39812=CARTESIAN_POINT('Ctrl Pts',(-0.0686305290079791,0.133885273559895,
0.0183317088352224));
#39813=CARTESIAN_POINT('Ctrl Pts',(-0.149752027927918,0.0149194227595303,
0.0262753655516404));
#39814=CARTESIAN_POINT('Ctrl Pts',(-0.0936553304388222,-0.117820164357962,
0.0342190222680582));
#39815=CARTESIAN_POINT('Ctrl Pts',(0.0482777357162085,-0.142534141023999,
0.0421626789844763));
#39816=CARTESIAN_POINT('Ctrl Pts',(0.145963511846947,-0.036655356268332,
0.050106335700894));
#39817=CARTESIAN_POINT('Ctrl Pts',(0.1098883156172,0.102829743898569,0.0580499924173122));
#39818=CARTESIAN_POINT('Ctrl Pts',(-0.0268917335099817,0.14807215694308,
0.0659936491337298));
#39819=CARTESIAN_POINT('Ctrl Pts',(-0.139027045104252,0.0576227776510703,
0.073937305850148));
#39820=CARTESIAN_POINT('Ctrl Pts',(-0.123755948978222,-0.0856352487256572,
0.0818809625665656));
#39821=CARTESIAN_POINT('Ctrl Pts',(0.00492741522215772,-0.150414534436879,
0.0898246192829839));
#39822=CARTESIAN_POINT('Ctrl Pts',(0.129095110802064,-0.0773519516565369,
0.0977682759994015));
#39823=CARTESIAN_POINT('Ctrl Pts',(0.134957883094489,0.0665976002541865,
0.10571193271582));
#39824=CARTESIAN_POINT('Ctrl Pts',(0.0171429060285707,0.14951580334048,
0.113655589432237));
#39825=CARTESIAN_POINT('Ctrl Pts',(-0.116382109817192,0.0954152433547932,
0.121599246148655));
#39826=CARTESIAN_POINT('Ctrl Pts',(-0.1432525695092,-0.046125529563486,
0.129542902865073));
#39827=CARTESIAN_POINT('Ctrl Pts',(-0.0388439106014103,-0.14539605120302,
0.137486559581491));
#39828=CARTESIAN_POINT('Ctrl Pts',(0.101161972846149,-0.111423147476419,
0.145430216297909));
#39829=CARTESIAN_POINT('Ctrl Pts',(0.148461288415133,0.0246598485140348,
0.153373873014327));
#39830=CARTESIAN_POINT('Ctrl Pts',(0.0597081294086373,0.138144132394173,
0.161317529730745));
#39831=CARTESIAN_POINT('Ctrl Pts',(-0.0837625843453943,0.125030763063784,
0.169261186447163));
#39832=CARTESIAN_POINT('Ctrl Pts',(-0.150471827652945,-0.00266294545074625,
0.177204843163581));
#39833=CARTESIAN_POINT('Ctrl Pts',(-0.0792861042094436,-0.127916284519489,
0.185148499879999));
#39834=CARTESIAN_POINT('Ctrl Pts',(0.0645587665352683,-0.13594494422742,
0.193092156596417));
#39835=CARTESIAN_POINT('Ctrl Pts',(0.149240875090081,-0.01939132254705,
0.201035813312835));
#39836=CARTESIAN_POINT('Ctrl Pts',(0.0971560830332309,0.114932840016463,
0.208979470029252));
#39837=CARTESIAN_POINT('Ctrl Pts',(-0.0439642118092888,0.143930574476409,
0.216923126745671));
#39838=CARTESIAN_POINT('Ctrl Pts',(-0.144794948028593,0.0410278589841287,
0.224866783462088));
#39839=CARTESIAN_POINT('Ctrl Pts',(-0.112933107548683,-0.0994734909739605,
0.232810440178506));
#39840=CARTESIAN_POINT('Ctrl Pts',(0.0224225719012751,-0.148815625715515,
0.240754096894924));
#39841=CARTESIAN_POINT('Ctrl Pts',(0.137229821435604,-0.0617805656840178,
0.248697753611342));
#39842=CARTESIAN_POINT('Ctrl Pts',(0.126277306185642,0.081871265594307,
0.25664141032776));
#39843=CARTESIAN_POINT('Ctrl Pts',(-0.000397900804215911,0.150494863242789,
0.264585067044178));
#39844=CARTESIAN_POINT('Ctrl Pts',(-0.126708464664056,0.0812023840164973,
0.272528723760596));
#39845=CARTESIAN_POINT('Ctrl Pts',(-0.136901215752127,-0.0625053542775162,
0.280472380477014));
#39846=CARTESIAN_POINT('Ctrl Pts',(-0.0216353419447375,-0.148932112608676,
0.288416037193432));
#39847=CARTESIAN_POINT('Ctrl Pts',(0.113457530724511,-0.0988749255844029,
0.29635969390985));
#39848=CARTESIAN_POINT('Ctrl Pts',(0.144575974027448,0.0417929410682694,
0.304303350626268));
#39849=CARTESIAN_POINT('Ctrl Pts',(0.0432025121524296,0.144161038870872,
0.312247007342686));
#39850=CARTESIAN_POINT('Ctrl Pts',(-0.0977624736752833,0.114417485240091,
0.320190664059103));
#39851=CARTESIAN_POINT('Ctrl Pts',(-0.149136249968981,-0.0201802166177978,
0.328134320775522));
#39852=CARTESIAN_POINT('Ctrl Pts',(-0.0638390058162424,-0.136284421348793,
0.336077977491939));
#39853=CARTESIAN_POINT('Ctrl Pts',(0.0799613992688094,-0.127495242353059,
0.344021634208357));
#39854=CARTESIAN_POINT('Ctrl Pts',(0.150483805397878,-0.00186723365027712,
0.351965290924775));
#39855=CARTESIAN_POINT('Ctrl Pts',(0.0831002675312467,0.125471939367544,
0.359908947641193));
#39856=CARTESIAN_POINT('Ctrl Pts',(-0.0604377810765522,0.137826473890756,
0.367852604357611));
#39857=CARTESIAN_POINT('Ctrl Pts',(-0.148589611907278,0.0238744586728436,
0.375796261074029));
#39858=CARTESIAN_POINT('Ctrl Pts',(-0.100571365962569,-0.111956515865154,
0.383739917790446));
#39859=CARTESIAN_POINT('Ctrl Pts',(0.0396121973075005,-0.145188625494464,
0.391683574506865));
#39860=CARTESIAN_POINT('Ctrl Pts',(0.143494480612217,-0.0453673691521286,
0.399627231223282));
#39861=CARTESIAN_POINT('Ctrl Pts',(0.115875923983247,0.0960292919722012,
0.407570887939701));
#39862=CARTESIAN_POINT('Ctrl Pts',(-0.0179332546906655,0.149423120517415,
0.415514544656118));
#39863=CARTESIAN_POINT('Ctrl Pts',(-0.135308213289508,0.0658829224797566,
0.423458201372536));
#39864=CARTESIAN_POINT('Ctrl Pts',(-0.128684169075867,-0.0780333019927274,
0.431401858088955));
#39865=CARTESIAN_POINT('Ctrl Pts',(-0.0041321849285115,-0.150438877221023,
0.439345514805372));
#39866=CARTESIAN_POINT('Ctrl Pts',(0.124207444980571,-0.0849789055356846,
0.44728917152179));
#39867=CARTESIAN_POINT('Ctrl Pts',(0.13871964211393,0.0583557185263908,
0.455232828238208));
#39868=CARTESIAN_POINT('Ctrl Pts',(0.0261098129416626,0.148214964857068,
0.463176484954626));
#39869=CARTESIAN_POINT('Ctrl Pts',(-0.110433266390416,0.10224214203642,
0.471120141671043));
#39870=CARTESIAN_POINT('Ctrl Pts',(-0.145762439740054,-0.0374170052831618,
0.479063798387463));
#39871=CARTESIAN_POINT('Ctrl Pts',(-0.0475332501860763,-0.142805819824299,
0.487007455103879));
#39872=CARTESIAN_POINT('Ctrl Pts',(0.0942958542259076,-0.117288323885235,
0.494951111820298));
#39873=CARTESIAN_POINT('Ctrl Pts',(0.149635107159208,0.0156445100139045,
0.502894768536715));
#39874=CARTESIAN_POINT('Ctrl Pts',(0.0679913965801436,0.134374014588598,
0.510838425253134));
#39875=CARTESIAN_POINT('Ctrl Pts',(-0.0762513070870269,0.129697499051486,
0.518782081969551));
#39876=CARTESIAN_POINT('Ctrl Pts',(-0.125384862498713,0.0477298987390752,
0.52407785311383));
#39877=CARTESIAN_POINT('Ctrl Pts',(-0.127184992207232,0.00540996832211942,
0.526725738685969));
#39878=CARTESIAN_POINT('Ctrl Pts',(0.0684664424539458,-0.0958295198918399,
-1.2490009027033E-16));
#39879=CARTESIAN_POINT('Ctrl Pts',(0.100353055357967,-0.0730477825951437,
0.00264788557213918));
#39880=CARTESIAN_POINT('Ctrl Pts',(0.139044776673305,0.00645180185613777,
0.00794365671641779));
#39881=CARTESIAN_POINT('Ctrl Pts',(0.0697747251423586,0.120597676732883,
0.0158873134328358));
#39882=CARTESIAN_POINT('Ctrl Pts',(-0.0634953696301243,0.123867541975778,
0.0238309701492536));
#39883=CARTESIAN_POINT('Ctrl Pts',(-0.138547094180758,0.0138031030283078,
0.0317746268656716));
#39884=CARTESIAN_POINT('Ctrl Pts',(-0.0866477340332458,-0.109004476490645,
0.0397182835820895));
#39885=CARTESIAN_POINT('Ctrl Pts',(0.0446654385229893,-0.131869273048715,
0.0476619402985074));
#39886=CARTESIAN_POINT('Ctrl Pts',(0.135042047193827,-0.033912683303242,
0.0556055970149253));
#39887=CARTESIAN_POINT('Ctrl Pts',(0.101666114468308,0.0951356880412728,
0.0635492537313433));
#39888=CARTESIAN_POINT('Ctrl Pts',(-0.0248796065525388,0.136992916606216,
0.0714929104477611));
#39889=CARTESIAN_POINT('Ctrl Pts',(-0.128624589451322,0.0533112540287094,
0.079436567164179));
#39890=CARTESIAN_POINT('Ctrl Pts',(-0.114496126401493,-0.079227740916452,
0.087380223880597));
#39891=CARTESIAN_POINT('Ctrl Pts',(0.00455872999049264,-0.139160029798142,
0.0953238805970148));
#39892=CARTESIAN_POINT('Ctrl Pts',(0.119435794773867,-0.0715642270726515,
0.103267537313433));
#39893=CARTESIAN_POINT('Ctrl Pts',(0.124859895376695,0.0616145512171006,
0.111211194029851));
#39894=CARTESIAN_POINT('Ctrl Pts',(0.0158602180480347,0.138328544685192,
0.119154850746269));
#39895=CARTESIAN_POINT('Ctrl Pts',(-0.107674021867399,0.0882759645413252,
0.127098507462686));
#39896=CARTESIAN_POINT('Ctrl Pts',(-0.132533946378209,-0.0426742674339329,
0.135042164179105));
#39897=CARTESIAN_POINT('Ctrl Pts',(-0.03593748288359,-0.134517045800752,
0.142985820895522));
#39898=CARTESIAN_POINT('Ctrl Pts',(0.0935927050428541,-0.103086105216301,
0.150929477611941));
#39899=CARTESIAN_POINT('Ctrl Pts',(0.137352931996012,0.0228147184504364,
0.158873134328358));
#39900=CARTESIAN_POINT('Ctrl Pts',(0.0552405729858772,0.127807739141585,
0.166816791044776));
#39901=CARTESIAN_POINT('Ctrl Pts',(-0.0774951953753252,0.115675554751273,
0.174760447761194));
#39902=CARTESIAN_POINT('Ctrl Pts',(-0.139213036149455,-0.00246369521179678,
0.182704104477612));
#39903=CARTESIAN_POINT('Ctrl Pts',(-0.0733536600413758,-0.118345172107485,
0.19064776119403));
#39904=CARTESIAN_POINT('Ctrl Pts',(0.0597282696676458,-0.12577310138558,
0.198591417910448));
#39905=CARTESIAN_POINT('Ctrl Pts',(0.138074187460599,-0.0179404007303906,
0.206535074626866));
#39906=CARTESIAN_POINT('Ctrl Pts',(0.0898865489335327,0.106333191146418,
0.214478731343283));
#39907=CARTESIAN_POINT('Ctrl Pts',(-0.0406746665030564,0.133161220808791,
0.222422388059702));
#39908=CARTESIAN_POINT('Ctrl Pts',(-0.133960919120719,0.0379580211457631,
0.230366044776119));
#39909=CARTESIAN_POINT('Ctrl Pts',(-0.104483085165326,-0.0920305608755558,
0.238309701492537));
#39910=CARTESIAN_POINT('Ctrl Pts',(0.0207448421498254,-0.137680756627218,
0.246253358208955));
#39911=CARTESIAN_POINT('Ctrl Pts',(0.126961839902422,-0.0571579428392388,
0.254197014925373));
#39912=CARTESIAN_POINT('Ctrl Pts',(0.116828827462796,0.075745391244066,
0.262140671641791));
#39913=CARTESIAN_POINT('Ctrl Pts',(-0.000368128572008151,0.139234348141551,
0.270084328358209));
#39914=CARTESIAN_POINT('Ctrl Pts',(-0.117227725261659,0.0751265575612168,
0.278027985074627));
#39915=CARTESIAN_POINT('Ctrl Pts',(-0.12665782156486,-0.0578285003930446,
0.285971641791045));
#39916=CARTESIAN_POINT('Ctrl Pts',(-0.0200165152988323,-0.137788527592198,
0.293915298507463));
#39917=CARTESIAN_POINT('Ctrl Pts',(0.104968269293632,-0.0914767820950745,
0.301858955223881));
#39918=CARTESIAN_POINT('Ctrl Pts',(0.133758329466478,0.0386658573002006,
0.309802611940298));
#39919=CARTESIAN_POINT('Ctrl Pts',(0.0399699596916912,0.133374441107753,
0.317746268656717));
#39920=CARTESIAN_POINT('Ctrl Pts',(-0.0904475674556682,0.10585639689043,
0.325689925373134));
#39921=CARTESIAN_POINT('Ctrl Pts',(-0.137977390731318,-0.0186702671811566,
0.333633582089553));
#39922=CARTESIAN_POINT('Ctrl Pts',(-0.0590623637863932,-0.126087177724698,
0.34157723880597));
#39923=CARTESIAN_POINT('Ctrl Pts',(0.0739784273282333,-0.117955633685244,
0.349520895522388));
#39924=CARTESIAN_POINT('Ctrl Pts',(0.139224117680559,-0.00172752115601949,
0.357464552238807));
#39925=CARTESIAN_POINT('Ctrl Pts',(0.0768824352591712,0.11608372080921,
0.365408208955224));
#39926=CARTESIAN_POINT('Ctrl Pts',(-0.0559156297430559,0.12751384888047,
0.373351865671643));
#39927=CARTESIAN_POINT('Ctrl Pts',(-0.137471653907146,0.0220880940313751,
0.381295522388059));
#39928=CARTESIAN_POINT('Ctrl Pts',(-0.0930462892870504,-0.103579565247593,
0.389239179104478));
#39929=CARTESIAN_POINT('Ctrl Pts',(0.0366482838797405,-0.134325140358292,
0.397182835820896));
#39930=CARTESIAN_POINT('Ctrl Pts',(0.132757756905765,-0.0419728350502109,
0.405126492537314));
#39931=CARTESIAN_POINT('Ctrl Pts',(0.107205710503746,0.0888440680441954,
0.413070149253731));
#39932=CARTESIAN_POINT('Ctrl Pts',(-0.0165914302528927,0.138242796692368,
0.42101380597015));
#39933=CARTESIAN_POINT('Ctrl Pts',(-0.125184012727194,0.0609533479579989,
0.428957462686568));
#39934=CARTESIAN_POINT('Ctrl Pts',(-0.119055601044071,-0.0721945965608292,
0.436901119402986));
#39935=CARTESIAN_POINT('Ctrl Pts',(-0.00382300141363195,-0.139182551176009,
0.444844776119403));
#39936=CARTESIAN_POINT('Ctrl Pts',(0.11491384000461,-0.0786205074584852,
0.452788432835821));
#39937=CARTESIAN_POINT('Ctrl Pts',(0.128340187352459,0.0539893538840985,
0.460732089552239));
#39938=CARTESIAN_POINT('Ctrl Pts',(0.024156191824071,0.137125039167645,
0.468675746268657));
#39939=CARTESIAN_POINT('Ctrl Pts',(-0.102170290252407,0.094592052461424,
0.476619402985075));
#39940=CARTESIAN_POINT('Ctrl Pts',(-0.13485601995589,-0.0346173432617789,
0.484563059701493));
#39941=CARTESIAN_POINT('Ctrl Pts',(-0.0439766578214066,-0.132120623957634,
0.492506716417911));
#39942=CARTESIAN_POINT('Ctrl Pts',(0.087240331747497,-0.108512430051717,
0.500450373134329));
#39943=CARTESIAN_POINT('Ctrl Pts',(0.138438921804208,0.0144739368962113,
0.508394029850746));
#39944=CARTESIAN_POINT('Ctrl Pts',(0.0629040591690992,0.12431971381125,
0.516337686567165));
#39945=CARTESIAN_POINT('Ctrl Pts',(-0.0705459363093062,0.119993110375402,
0.524281343283582));
#39946=CARTESIAN_POINT('Ctrl Pts',(-0.116003159314893,0.0441585924901374,
0.529577114427861));
#39947=CARTESIAN_POINT('Ctrl Pts',(-0.117668597464311,0.00500517689817385,
0.532225));
#39948=CARTESIAN_POINT('',(0.0684664424539457,-0.0958295198918399,0.));
#39949=CARTESIAN_POINT('Ctrl Pts',(0.0684664424539458,-0.0958295198918399,
-1.2490009027033E-16));
#39950=CARTESIAN_POINT('Ctrl Pts',(0.100353055357967,-0.0730477825951437,
0.00264788557213918));
#39951=CARTESIAN_POINT('Ctrl Pts',(0.139044776673305,0.00645180185613777,
0.00794365671641779));
#39952=CARTESIAN_POINT('Ctrl Pts',(0.0697747251423586,0.120597676732883,
0.0158873134328358));
#39953=CARTESIAN_POINT('Ctrl Pts',(-0.0634953696301243,0.123867541975778,
0.0238309701492536));
#39954=CARTESIAN_POINT('Ctrl Pts',(-0.116013612970437,0.0468487789511056,
0.0293896285137698));
#39955=CARTESIAN_POINT('Ctrl Pts',(-0.117946226519694,0.00395164958315818,
0.0323004013061468));
#39956=CARTESIAN_POINT('Ctrl Pts',(-0.117919967015755,7.48285734863559E-5,
0.0325632885263843));
#39957=CARTESIAN_POINT('Ctrl Pts',(0.0635548502597316,0.132093933345895,
7.26415455565288E-18));
#39958=CARTESIAN_POINT('Ctrl Pts',(0.0667625318922158,0.13018322972067,
8.97431508554919E-18));
#39959=CARTESIAN_POINT('Ctrl Pts',(0.0698866263065284,0.128144700630429,
-1.82766240468292E-17));
#39960=CARTESIAN_POINT('Ctrl Pts',(0.0729183991770622,0.125977863427922,
-1.55040910665427E-17));
#39961=CARTESIAN_POINT('Ctrl Pts',(0.0787736058599248,0.121793090949712,
-9.35723626730848E-18));
#39962=CARTESIAN_POINT('Ctrl Pts',(0.0842851176408076,0.117130107773036,
-2.42858544627756E-17));
#39963=CARTESIAN_POINT('Ctrl Pts',(0.0894225077026563,0.112048986470911,
-3.0140820395097E-17));
#39964=CARTESIAN_POINT('Ctrl Pts',(0.0927550575340165,0.108752937361409,
-3.39388512036349E-17));
#39965=CARTESIAN_POINT('Ctrl Pts',(0.095930929613759,0.105278801629612,
-4.52445550988079E-17));
#39966=CARTESIAN_POINT('Ctrl Pts',(0.0989262797420343,0.101660133512415,
-3.46944695195361E-17));
#39967=CARTESIAN_POINT('Ctrl Pts',(0.103069367071931,0.0966548895891983,
-2.01018763264428E-17));
#39968=CARTESIAN_POINT('Ctrl Pts',(0.106874603061403,0.0913668016366946,
-3.77038544403596E-17));
#39969=CARTESIAN_POINT('Ctrl Pts',(0.110317478847291,0.0858396385675292,
-3.33934269125535E-17));
#39970=CARTESIAN_POINT('Ctrl Pts',(0.112268215177796,0.082707943300496,
-3.09511350317464E-17));
#39971=CARTESIAN_POINT('Ctrl Pts',(0.114103333501928,0.079497785539906,
-4.97099315558713E-17));
#39972=CARTESIAN_POINT('Ctrl Pts',(0.115814486180912,0.0762220963964089,
-4.59701721133854E-17));
#39973=CARTESIAN_POINT('Ctrl Pts',(0.120425861906472,0.0673944601566279,
-3.58919154362862E-17));
#39974=CARTESIAN_POINT('Ctrl Pts',(0.124112940735196,0.0581470311761757,
-7.4029188042833E-18));
#39975=CARTESIAN_POINT('Ctrl Pts',(0.126786742395323,0.0486381528803429,
-1.99493199737333E-17));
#39976=CARTESIAN_POINT('Ctrl Pts',(0.128289456800478,0.0432940285927791,
-2.70005751402403E-17));
#39977=CARTESIAN_POINT('Ctrl Pts',(0.129471235246761,0.0378670663167402,
-8.81130640021771E-18));
#39978=CARTESIAN_POINT('Ctrl Pts',(0.130308765287913,0.0323855967712197,
-1.47451495458029E-17));
#39979=CARTESIAN_POINT('Ctrl Pts',(0.130909407220836,0.0284545133457784,
-1.90006566219738E-17));
#39980=CARTESIAN_POINT('Ctrl Pts',(0.131332629221345,0.0244917931761562,
-4.99383881545994E-18));
#39981=CARTESIAN_POINT('Ctrl Pts',(0.1315678106143,0.0205341495544984,-6.07153216591882E-18));
#39982=CARTESIAN_POINT('Ctrl Pts',(0.131851015138327,0.015768370408227,
-7.36928633144951E-18));
#39983=CARTESIAN_POINT('Ctrl Pts',(0.131863254926577,0.0110027231344166,
-1.87693227394301E-17));
#39984=CARTESIAN_POINT('Ctrl Pts',(0.131591710623677,0.00625556877829329,
-1.38777878078145E-17));
#39985=CARTESIAN_POINT('Ctrl Pts',(0.131146495407245,-0.00152771126671145,
-5.8577860622257E-18));
#39986=CARTESIAN_POINT('Ctrl Pts',(0.12993932260643,-0.00926206422336292,
-1.85374582714576E-17));
#39987=CARTESIAN_POINT('Ctrl Pts',(0.128016835267175,-0.0168585737917118,
-1.04083408558608E-17));
#39988=CARTESIAN_POINT('Ctrl Pts',(0.126984115402176,-0.0209392593575938,
-6.04154952851233E-18));
#39989=CARTESIAN_POINT('Ctrl Pts',(0.125742427413826,-0.0249846391579523,
1.89772622437785E-17));
#39990=CARTESIAN_POINT('Ctrl Pts',(0.124308621487175,-0.0289511201777135,
1.38777878078145E-17));
#39991=CARTESIAN_POINT('Ctrl Pts',(0.121785637190381,-0.0359307044717815,
4.90454136999372E-18));
#39992=CARTESIAN_POINT('Ctrl Pts',(0.118666317325564,-0.042682712152767,
2.07260850608487E-18));
#39993=CARTESIAN_POINT('Ctrl Pts',(0.114994151346376,-0.0491304207397526,
8.67361737988404E-18));
#39994=CARTESIAN_POINT('Ctrl Pts',(0.112470213235982,-0.0535620334499726,
1.32105958166033E-17));
#39995=CARTESIAN_POINT('Ctrl Pts',(0.109684704250007,-0.0578497076893306,
-2.69424258846107E-17));
#39996=CARTESIAN_POINT('Ctrl Pts',(0.106648013733876,-0.0619641182107045,
-2.60208521396521E-17));
#39997=CARTESIAN_POINT('Ctrl Pts',(0.104460102807982,-0.0649285176730499,
-2.53568657192706E-17));
#39998=CARTESIAN_POINT('Ctrl Pts',(0.102139560475227,-0.0678046962501359,
-1.87244270863087E-17));
#39999=CARTESIAN_POINT('Ctrl Pts',(0.0997061632112326,-0.0705633954799611,
-1.90819582357449E-17));
#40000=CARTESIAN_POINT('Ctrl Pts',(0.0939222145804643,-0.0771205552455056,
-1.9931775005426E-17));
#40001=CARTESIAN_POINT('Ctrl Pts',(0.087486631308301,-0.0830406987797476,
-2.77894727952103E-19));
#40002=CARTESIAN_POINT('Ctrl Pts',(0.0804584136226653,-0.0881761753022089,
-1.73472347597681E-18));
#40003=CARTESIAN_POINT('Ctrl Pts',(0.0766344364937381,-0.0909703324621629,
-2.52736822068868E-18));
#40004=CARTESIAN_POINT('Ctrl Pts',(0.0726345968903183,-0.0935314830199203,
-1.19936303452846E-17));
#40005=CARTESIAN_POINT('Ctrl Pts',(0.0684664424539472,-0.0958295198918389,
-1.04083408558608E-17));
#40006=CARTESIAN_POINT('Ctrl Pts',(-0.00157033164522019,0.146071601053478,
0.50365));
#40007=CARTESIAN_POINT('Ctrl Pts',(0.0218930565124332,0.146360870028846,
0.502379967541691));
#40008=CARTESIAN_POINT('Ctrl Pts',(0.0454120282149095,0.141318853716995,
0.501109935083381));
#40009=CARTESIAN_POINT('Ctrl Pts',(0.0661716191392787,0.130837066204352,
0.499839902625071));
#40010=CARTESIAN_POINT('Ctrl Pts',(0.109453206891224,0.108983629511958,
0.497192017052932));
#40011=CARTESIAN_POINT('Ctrl Pts',(0.140740342380216,0.0634846428806245,
0.494544131480792));
#40012=CARTESIAN_POINT('Ctrl Pts',(0.145780480343632,0.0152641882646972,
0.491896245908653));
#40013=CARTESIAN_POINT('Ctrl Pts',(0.150820618307048,-0.0329562663512301,
0.489248360336514));
#40014=CARTESIAN_POINT('Ctrl Pts',(0.129613758744889,-0.0838981889517511,
0.486600474764375));
#40015=CARTESIAN_POINT('Ctrl Pts',(0.0918347732807851,-0.114258500252904,
0.483952589192235));
#40016=CARTESIAN_POINT('Ctrl Pts',(0.0540557878166811,-0.144618811554058,
0.481304703620096));
#40017=CARTESIAN_POINT('Ctrl Pts',(-0.000295323549367926,-0.154397511555843,
0.478656818047957));
#40018=CARTESIAN_POINT('Ctrl Pts',(-0.0462923532978867,-0.139093547851452,
0.476008932475817));
#40019=CARTESIAN_POINT('Ctrl Pts',(-0.0922893830464049,-0.123789584147061,
0.473361046903678));
#40020=CARTESIAN_POINT('Ctrl Pts',(-0.129932331177393,-0.0834029567364939,
0.470713161331538));
#40021=CARTESIAN_POINT('Ctrl Pts',(-0.141984461802563,-0.0364498679458208,
0.468065275759399));
#40022=CARTESIAN_POINT('Ctrl Pts',(-0.145018518318758,-0.0246296902999453,
0.467398685367696));
#40023=CARTESIAN_POINT('Ctrl Pts',(-0.146430750426956,-0.0123933615350992,
0.466732094975993));
#40024=CARTESIAN_POINT('Ctrl Pts',(-0.146320034481408,-0.000132042578932776,
0.466065504584291));
#40025=CARTESIAN_POINT('Origin',(0.,0.,-0.0924367114736154));
#40026=CARTESIAN_POINT('',(-0.0684664424539447,-0.0958295198918406,0.));
#40027=CARTESIAN_POINT('Ctrl Pts',(-0.0686153921261821,-0.095961513397809,
-8.6871699070401E-17));
#40028=CARTESIAN_POINT('Ctrl Pts',(-0.0390777571216276,-0.11683521110507,
0.00245324280107157));
#40029=CARTESIAN_POINT('Ctrl Pts',(0.0440758903380829,-0.130444567971902,
0.00755732030717748));
#40030=CARTESIAN_POINT('Ctrl Pts',(0.134343829836486,-0.03677094505856,
0.0153122325183177));
#40031=CARTESIAN_POINT('Ctrl Pts',(0.103577487134497,0.0931457228401511,
0.0232647366334205));
#40032=CARTESIAN_POINT('Ctrl Pts',(-0.022319455813322,0.137480661654608,
0.0312172407485234));
#40033=CARTESIAN_POINT('Ctrl Pts',(-0.107013184840641,0.0716760847082379,
0.0376078990285884));
#40034=CARTESIAN_POINT('Ctrl Pts',(-0.117673522927843,0.0162276125558733,
0.0413477226036194));
#40035=CARTESIAN_POINT('Ctrl Pts',(-0.117605093279175,5.6374090473453E-5,
0.042436711473616));
#40036=CARTESIAN_POINT('Origin',(0.,0.,0.));
#40037=CARTESIAN_POINT('Ctrl Pts',(-0.0510216505388437,0.106149619882937,
-0.0164977839420935));
#40038=CARTESIAN_POINT('Ctrl Pts',(-0.0863815445949669,0.0891536084077042,
-0.0138469492370593));
#40039=CARTESIAN_POINT('Ctrl Pts',(-0.138162556478479,0.0173380738482791,
-0.00854527982699074));
#40040=CARTESIAN_POINT('Ctrl Pts',(-0.0892152289856901,-0.107087400898305,
-0.000592775711887911));
#40041=CARTESIAN_POINT('Ctrl Pts',(0.0417759011768067,-0.132831332515275,
0.00735972840321487));
#40042=CARTESIAN_POINT('Ctrl Pts',(0.134343829836486,-0.03677094505856,
0.0153122325183177));
#40043=CARTESIAN_POINT('Ctrl Pts',(0.103577487134497,0.0931457228401511,
0.0232647366334205));
#40044=CARTESIAN_POINT('Ctrl Pts',(-0.022319455813322,0.137480661654608,
0.0312172407485234));
#40045=CARTESIAN_POINT('Ctrl Pts',(-0.127711920735776,0.0555937658099327,
0.0391697448636261));
#40046=CARTESIAN_POINT('Ctrl Pts',(-0.115832853027164,-0.0773572203301017,
0.047122248978729));
#40047=CARTESIAN_POINT('Ctrl Pts',(0.00241643506700816,-0.139265216174241,
0.0550747530938317));
#40048=CARTESIAN_POINT('Ctrl Pts',(0.118445458723555,-0.0732914200146354,
0.0630272572089346));
#40049=CARTESIAN_POINT('Ctrl Pts',(0.125708256673902,0.0599868231457294,
0.0709797613240373));
#40050=CARTESIAN_POINT('Ctrl Pts',(0.0175344664057042,0.138178956948752,
0.0789322654391402));
#40051=CARTESIAN_POINT('Ctrl Pts',(-0.106740805893122,0.0894837054538652,
0.0868847695542431));
#40052=CARTESIAN_POINT('Ctrl Pts',(-0.132997503503664,-0.0413835288220579,
0.0948372736693457));
#40053=CARTESIAN_POINT('Ctrl Pts',(-0.0371242974264225,-0.134248668971966,
0.102789777784449));
#40054=CARTESIAN_POINT('Ctrl Pts',(0.0928396337021713,-0.10383510521762,
0.110742281899551));
#40055=CARTESIAN_POINT('Ctrl Pts',(0.137550169005636,0.0219289054269618,
0.118694786014654));
#40056=CARTESIAN_POINT('Ctrl Pts',(0.0559501922162531,0.127555870431356,
0.126647290129757));
#40057=CARTESIAN_POINT('Ctrl Pts',(-0.0770281035821754,0.116049974518826,
0.13459979424486));
#40058=CARTESIAN_POINT('Ctrl Pts',(-0.13927251071013,-0.00202308703008076,
0.142552298359963));
#40059=CARTESIAN_POINT('Ctrl Pts',(-0.0736248085349355,-0.118238371369349,
0.150504802475065));
#40060=CARTESIAN_POINT('Ctrl Pts',(0.0596315829014974,-0.125876921640408,
0.158457306590168));
#40061=CARTESIAN_POINT('Ctrl Pts',(0.138129079193178,-0.0179243554725553,
0.166409810705271));
#40062=CARTESIAN_POINT('Ctrl Pts',(0.0897844651888838,0.106487909275724,
0.174362314820374));
#40063=CARTESIAN_POINT('Ctrl Pts',(-0.0410080379701501,0.133113732800722,
0.182314818935477));
#40064=CARTESIAN_POINT('Ctrl Pts',(-0.134143401206605,0.0375029724551737,
0.190267323050579));
#40065=CARTESIAN_POINT('Ctrl Pts',(-0.104096649768354,-0.0925462723956308,
0.198219827165683));
#40066=CARTESIAN_POINT('Ctrl Pts',(0.0215406810767683,-0.137611496939632,
0.206172331280785));
#40067=CARTESIAN_POINT('Ctrl Pts',(0.127397488829925,-0.056309900280862,
0.214124835395888));
#40068=CARTESIAN_POINT('Ctrl Pts',(0.116266864218555,0.0767003345124148,
0.222077339510991));
#40069=CARTESIAN_POINT('Ctrl Pts',(-0.0016300870944122,0.139277664563073,
0.230029843626094));
#40070=CARTESIAN_POINT('Ctrl Pts',(-0.1180301509465,0.0739581536911037,
0.237982347741196));
#40071=CARTESIAN_POINT('Ctrl Pts',(-0.126044685167542,-0.0592761534753867,
0.245934851856299));
#40072=CARTESIAN_POINT('Ctrl Pts',(-0.0183140487741412,-0.138077951344142,
0.253887355971402));
#40073=CARTESIAN_POINT('Ctrl Pts',(0.106234136865658,-0.0900845891054932,
0.261839860086505));
#40074=CARTESIAN_POINT('Ctrl Pts',(0.133228916899009,0.040632262203075,
0.269792364201608));
#40075=CARTESIAN_POINT('Ctrl Pts',(0.0378813411502606,0.134037043471229,
0.27774486831671));
#40076=CARTESIAN_POINT('Ctrl Pts',(-0.092252170148986,0.104357376993109,
0.285697372431813));
#40077=CARTESIAN_POINT('Ctrl Pts',(-0.137671731315388,-0.021152291274371,
0.293649876546916));
#40078=CARTESIAN_POINT('Ctrl Pts',(-0.0566691588697243,-0.127238089669758,
0.301602380662019));
#40079=CARTESIAN_POINT('Ctrl Pts',(0.0763719541489209,-0.116482829853556,
0.309554884777122));
#40080=CARTESIAN_POINT('Ctrl Pts',(0.139281709756163,0.00123707506708643,
0.317507388892225));
#40081=CARTESIAN_POINT('Ctrl Pts',(0.0742909098282569,0.117820990265484,
0.325459893007327));
#40082=CARTESIAN_POINT('Ctrl Pts',(-0.0589202520252667,0.1262114453589,
0.33341239712243));
#40083=CARTESIAN_POINT('Ctrl Pts',(-0.13802572406761,0.0187035960922139,
0.341364901237533));
#40084=CARTESIAN_POINT('Ctrl Pts',(-0.0903839958430062,-0.105979518461414,
0.349317405352636));
#40085=CARTESIAN_POINT('Ctrl Pts',(0.0402561631274929,-0.133343040355529,
0.357269909467738));
#40086=CARTESIAN_POINT('Ctrl Pts',(0.133929618074243,-0.0382594079720193,
0.365222413582842));
#40087=CARTESIAN_POINT('Ctrl Pts',(0.104617274119081,0.0919573329132998,
0.373174917697944));
#40088=CARTESIAN_POINT('Ctrl Pts',(-0.020763734615072,0.137730870367254,
0.381127421813047));
#40089=CARTESIAN_POINT('Ctrl Pts',(-0.127077674436729,0.0570279646339328,
0.38907992592815));
#40090=CARTESIAN_POINT('Ctrl Pts',(-0.116697873675526,-0.0760429626350431,
0.397032430043252));
#40091=CARTESIAN_POINT('Ctrl Pts',(0.000844063931402275,-0.139284651766041,
0.404984934158356));
#40092=CARTESIAN_POINT('Ctrl Pts',(0.117610871049501,-0.0746230633995127,
0.412937438273457));
#40093=CARTESIAN_POINT('Ctrl Pts',(0.126377239427685,0.0585638604483229,
0.420889942388562));
#40094=CARTESIAN_POINT('Ctrl Pts',(0.0190929207373193,0.137972437690235,
0.428842446503664));
#40095=CARTESIAN_POINT('Ctrl Pts',(-0.105723916050958,0.0906826070998613,
0.436794950618767));
#40096=CARTESIAN_POINT('Ctrl Pts',(-0.133456368516637,-0.0398795994144927,
0.44474745473387));
#40097=CARTESIAN_POINT('Ctrl Pts',(-0.038636663810782,-0.133821400192823,
0.452699958848972));
#40098=CARTESIAN_POINT('Ctrl Pts',(0.0916608011058181,-0.104875817685159,
0.460652462964076));
#40099=CARTESIAN_POINT('Ctrl Pts',(0.137790741908166,0.0203740232160909,
0.468604967079177));
#40100=CARTESIAN_POINT('Ctrl Pts',(0.0573828398023632,0.126918127906013,
0.476557471194281));
#40101=CARTESIAN_POINT('Ctrl Pts',(-0.0757067578384881,0.11690841395886,
0.484509975309383));
#40102=CARTESIAN_POINT('Ctrl Pts',(-0.139299045817393,-0.000444250914572553,
0.492462479424487));
#40103=CARTESIAN_POINT('Ctrl Pts',(-0.0749307309976486,-0.117412744486246,
0.500414983539588));
#40104=CARTESIAN_POINT('Ctrl Pts',(0.0581614397283287,-0.126517333775439,
0.508367487654693));
#40105=CARTESIAN_POINT('Ctrl Pts',(0.138005962114904,-0.01953005209576,
0.516319991769794));
#40106=CARTESIAN_POINT('Ctrl Pts',(0.0908022345067483,0.105567300931769,
0.524272495884898));
#40107=CARTESIAN_POINT('Ctrl Pts',(0.00421962447768953,0.124065836989857,
0.529574165294966));
#40108=CARTESIAN_POINT('Ctrl Pts',(-0.0334019664626881,0.11293918390632,
0.532225));
#40109=CARTESIAN_POINT('Ctrl Pts',(-0.0551480035117362,0.114734422509853,
-0.0109985226280624));
#40110=CARTESIAN_POINT('Ctrl Pts',(-0.0933676130497917,0.096363866272985,
-0.0083476879230281));
#40111=CARTESIAN_POINT('Ctrl Pts',(-0.149336390912421,0.0187402827500406,
-0.00304601851295955));
#40112=CARTESIAN_POINT('Ctrl Pts',(-0.0964304703874203,-0.115748046141832,
0.00490648560214325));
#40113=CARTESIAN_POINT('Ctrl Pts',(0.0451545083405425,-0.143574006615959,
0.0128589897172461));
#40114=CARTESIAN_POINT('Ctrl Pts',(0.145208826475777,-0.0397447786538297,
0.0208114938323489));
#40115=CARTESIAN_POINT('Ctrl Pts',(0.1119542696856,0.100678841159424,0.0287639979474517));
#40116=CARTESIAN_POINT('Ctrl Pts',(-0.0241245317345429,0.148599348152253,
0.0367165020625545));
#40117=CARTESIAN_POINT('Ctrl Pts',(-0.138040564718016,0.060089886543023,
0.0446690061776573));
#40118=CARTESIAN_POINT('Ctrl Pts',(-0.125200782766784,-0.0836134506306251,
0.0526215102927601));
#40119=CARTESIAN_POINT('Ctrl Pts',(0.00261186316306541,-0.150528227713698,
0.0605740144078629));
#40120=CARTESIAN_POINT('Ctrl Pts',(0.128024681770397,-0.0792188305486153,
0.0685265185229658));
#40121=CARTESIAN_POINT('Ctrl Pts',(0.135874855228935,0.0648382304092657,
0.0764790226380685));
#40122=CARTESIAN_POINT('Ctrl Pts',(0.0189525584669602,0.149354117763329,
0.0844315267531714));
#40123=CARTESIAN_POINT('Ctrl Pts',(-0.115373420421943,0.096720659768857,
0.0923840308682741));
#40124=CARTESIAN_POINT('Ctrl Pts',(-0.143753616608078,-0.0447304030485916,
0.100336534983377));
#40125=CARTESIAN_POINT('Ctrl Pts',(-0.0401267082350556,-0.145105969519263,
0.10828903909848));
#40126=CARTESIAN_POINT('Ctrl Pts',(0.100347997200478,-0.112232722514991,
0.116241543213583));
#40127=CARTESIAN_POINT('Ctrl Pts',(0.148674476878943,0.0237023957618521,
0.124194047328685));
#40128=CARTESIAN_POINT('Ctrl Pts',(0.0604751387741805,0.137871893915615,
0.132146551443788));
#40129=CARTESIAN_POINT('Ctrl Pts',(-0.0832577167141655,0.125435463861147,
0.140099055558891));
#40130=CARTESIAN_POINT('Ctrl Pts',(-0.150536112191887,-0.00218670328107987,
0.148051559673994));
#40131=CARTESIAN_POINT('Ctrl Pts',(-0.0795791817151125,-0.127800846319831,
0.156004063789097));
#40132=CARTESIAN_POINT('Ctrl Pts',(0.0644542602705204,-0.136057160898527,
0.163956567904199));
#40133=CARTESIAN_POINT('Ctrl Pts',(0.149300206166772,-0.0193739796362248,
0.171909072019302));
#40134=CARTESIAN_POINT('Ctrl Pts',(0.0970457433117808,0.115100070904688,
0.179861576134405));
#40135=CARTESIAN_POINT('Ctrl Pts',(-0.0443245445434091,0.143879245897109,
0.187814080249508));
#40136=CARTESIAN_POINT('Ctrl Pts',(-0.144992188270862,0.0405360084359473,
0.195766584364611));
#40137=CARTESIAN_POINT('Ctrl Pts',(-0.11251541936329,-0.100030910430598,
0.203719088479714));
#40138=CARTESIAN_POINT('Ctrl Pts',(0.023282773942454,-0.148740764681937,
0.211671592594816));
#40139=CARTESIAN_POINT('Ctrl Pts',(0.13770070327361,-0.0608639380662604,
0.219624096709919));
#40140=CARTESIAN_POINT('Ctrl Pts',(0.125669894417509,0.0829034394687354,
0.227576600825022));
#40141=CARTESIAN_POINT('Ctrl Pts',(-0.00176191965288545,0.150541682860363,
0.235529104940125));
#40142=CARTESIAN_POINT('Ctrl Pts',(-0.127575786164206,0.0799394860104231,
0.243481609055227));
#40143=CARTESIAN_POINT('Ctrl Pts',(-0.136238492225245,-0.0640700856498972,
0.25143411317033));
#40144=CARTESIAN_POINT('Ctrl Pts',(-0.0197951892077968,-0.149244943376008,
0.259386617285433));
#40145=CARTESIAN_POINT('Ctrl Pts',(0.114825774765427,-0.0973701396147685,
0.267339121400536));
#40146=CARTESIAN_POINT('Ctrl Pts',(0.144003745457388,0.0439183780806738,
0.275291625515639));
#40147=CARTESIAN_POINT('Ctrl Pts',(0.0409449775285778,0.144877228901612,
0.283244129630741));
#40148=CARTESIAN_POINT('Ctrl Pts',(-0.0997130227974173,0.112797232784741,
0.291196633745845));
#40149=CARTESIAN_POINT('Ctrl Pts',(-0.148805870485663,-0.0228629732899794,
0.299149137860947));
#40150=CARTESIAN_POINT('Ctrl Pts',(-0.0612522515314454,-0.137528412778265,
0.30710164197605));
#40151=CARTESIAN_POINT('Ctrl Pts',(0.0825485014914671,-0.125903326175825,
0.315054146091153));
#40152=CARTESIAN_POINT('Ctrl Pts',(0.150546055206619,0.00133712295512629,
0.323006650206255));
#40153=CARTESIAN_POINT('Ctrl Pts',(0.0802991536500716,0.12734970970746,
0.330959154321359));
#40154=CARTESIAN_POINT('Ctrl Pts',(-0.0636854008305359,0.136418739071857,
0.338911658436461));
#40155=CARTESIAN_POINT('Ctrl Pts',(-0.149188492242044,0.0202162409895048,
0.346864162551565));
#40156=CARTESIAN_POINT('Ctrl Pts',(-0.0976937607371238,-0.114550564212591,
0.354816666666667));
#40157=CARTESIAN_POINT('Ctrl Pts',(0.0435118621620017,-0.144127098596976,
0.36276917078177));
#40158=CARTESIAN_POINT('Ctrl Pts',(0.144761115524102,-0.041353620334011,
0.370721674896872));
#40159=CARTESIAN_POINT('Ctrl Pts',(0.113078148973544,0.0993943407332879,
0.378674179011976));
#40160=CARTESIAN_POINT('Ctrl Pts',(-0.0224429922861266,0.148869792381672,
0.386626683127078));
#40161=CARTESIAN_POINT('Ctrl Pts',(-0.137355024035624,0.0616400755499871,
0.394579187242181));
#40162=CARTESIAN_POINT('Ctrl Pts',(-0.126135761569897,-0.0821929029373033,
0.402531691357283));
#40163=CARTESIAN_POINT('Ctrl Pts',(0.000912327221120078,-0.150549235150219,
0.410484195472387));
#40164=CARTESIAN_POINT('Ctrl Pts',(0.127122597194663,-0.0806581699915775,
0.418436699587489));
#40165=CARTESIAN_POINT('Ctrl Pts',(0.136597941661171,0.0633001862455649,
0.426389203702593));
#40166=CARTESIAN_POINT('Ctrl Pts',(0.0206370520896696,0.149130896352934,
0.434341707817695));
#40167=CARTESIAN_POINT('Ctrl Pts',(-0.114274290072485,0.0980165220446819,
0.442294211932798));
#40168=CARTESIAN_POINT('Ctrl Pts',(-0.144249592121994,-0.0431048440285699,
0.450246716047901));
#40169=CARTESIAN_POINT('Ctrl Pts',(-0.0417613865685641,-0.144644145570336,
0.458199220163003));
#40170=CARTESIAN_POINT('Ctrl Pts',(0.0990738270496334,-0.113357602133906,
0.466151724278107));
#40171=CARTESIAN_POINT('Ctrl Pts',(0.148934506006449,0.0220217631535408,
0.474104228393209));
#40172=CARTESIAN_POINT('Ctrl Pts',(0.0620236510875902,0.137182574251203,
0.482056732508312));
#40173=CARTESIAN_POINT('Ctrl Pts',(-0.0818295077294796,0.126363329203676,
0.490009236623415));
#40174=CARTESIAN_POINT('Ctrl Pts',(-0.150564793313981,-0.000480179506898605,
0.497961740738518));
#40175=CARTESIAN_POINT('Ctrl Pts',(-0.0809907200679325,-0.126908447234973,
0.50591424485362));
#40176=CARTESIAN_POINT('Ctrl Pts',(0.0628652199313619,-0.136749366076106,
0.513866748968723));
#40177=CARTESIAN_POINT('Ctrl Pts',(0.149167132050327,-0.0211095362495466,
0.521819253083827));
#40178=CARTESIAN_POINT('Ctrl Pts',(0.0981458242641405,0.114105008776176,
0.529771757198928));
#40179=CARTESIAN_POINT('Ctrl Pts',(0.00456088470396912,0.134099605593792,
0.535073426608997));
#40180=CARTESIAN_POINT('Ctrl Pts',(-0.0361033354336669,0.122073089461044,
0.537724261314032));
#40181=CARTESIAN_POINT('Ctrl Pts',(-0.0592743564846287,0.123319225136769,
-0.00549926131403118));
#40182=CARTESIAN_POINT('Ctrl Pts',(-0.100353681504617,0.103574124138266,
-0.00284842660899691));
#40183=CARTESIAN_POINT('Ctrl Pts',(-0.160510225346362,0.0201424916518021,
0.00245324280107164));
#40184=CARTESIAN_POINT('Ctrl Pts',(-0.103645711789151,-0.124408691385358,
0.0104057469161744));
#40185=CARTESIAN_POINT('Ctrl Pts',(0.0485331155042784,-0.154316680716642,
0.0183582510312773));
#40186=CARTESIAN_POINT('Ctrl Pts',(0.156073823115068,-0.0427186122490994,
0.02631075514638));
#40187=CARTESIAN_POINT('Ctrl Pts',(0.120331052236703,0.108211959478697,
0.0342632592614829));
#40188=CARTESIAN_POINT('Ctrl Pts',(-0.0259296076557639,0.159718034649898,
0.0422157633765857));
#40189=CARTESIAN_POINT('Ctrl Pts',(-0.148369208700255,0.0645860072761131,
0.0501682674916885));
#40190=CARTESIAN_POINT('Ctrl Pts',(-0.134568712506405,-0.0898696809311483,
0.0581207716067913));
#40191=CARTESIAN_POINT('Ctrl Pts',(0.00280729125912282,-0.161791239253156,
0.0660732757218941));
#40192=CARTESIAN_POINT('Ctrl Pts',(0.137603904817239,-0.0851462410825952,
0.074025779836997));
#40193=CARTESIAN_POINT('Ctrl Pts',(0.146041453783967,0.0696896376728019,
0.0819782839520996));
#40194=CARTESIAN_POINT('Ctrl Pts',(0.0203706505282163,0.160529278577907,
0.0899307880672026));
#40195=CARTESIAN_POINT('Ctrl Pts',(-0.124006034950765,0.103957614083849,
0.0978832921823053));
#40196=CARTESIAN_POINT('Ctrl Pts',(-0.154509729712493,-0.0480772772751253,
0.105835796297408));
#40197=CARTESIAN_POINT('Ctrl Pts',(-0.0431291190436888,-0.155963270066561,
0.113788300412511));
#40198=CARTESIAN_POINT('Ctrl Pts',(0.107856360698785,-0.120630339812362,
0.121740804527614));
#40199=CARTESIAN_POINT('Ctrl Pts',(0.159798784752249,0.0254758860967424,
0.129693308642717));
#40200=CARTESIAN_POINT('Ctrl Pts',(0.065000085332108,0.148187917399874,
0.137645812757819));
#40201=CARTESIAN_POINT('Ctrl Pts',(-0.0894873298461556,0.134820953203468,
0.145598316872922));
#40202=CARTESIAN_POINT('Ctrl Pts',(-0.161799713673645,-0.00235031953207901,
0.153550820988025));
#40203=CARTESIAN_POINT('Ctrl Pts',(-0.0855335548952896,-0.137363321270313,
0.161503325103128));
#40204=CARTESIAN_POINT('Ctrl Pts',(0.0692769376395434,-0.146237400156646,
0.169455829218231));
#40205=CARTESIAN_POINT('Ctrl Pts',(0.160471333140366,-0.0208236037998943,
0.177408333333334));
#40206=CARTESIAN_POINT('Ctrl Pts',(0.104307021434678,0.123712232533651,
0.185360837448436));
#40207=CARTESIAN_POINT('Ctrl Pts',(-0.0476410511166683,0.154644758993495,
0.193313341563539));
#40208=CARTESIAN_POINT('Ctrl Pts',(-0.155840975335119,0.043569044416721,
0.201265845678642));
#40209=CARTESIAN_POINT('Ctrl Pts',(-0.120934188958227,-0.107515548465566,
0.209218349793745));
#40210=CARTESIAN_POINT('Ctrl Pts',(0.0250248668081396,-0.159870032424242,
0.217170853908847));
#40211=CARTESIAN_POINT('Ctrl Pts',(0.148003917717295,-0.0654179758516589,
0.22512335802395));
#40212=CARTESIAN_POINT('Ctrl Pts',(0.135072924616463,0.0891065444250562,
0.233075862139053));
#40213=CARTESIAN_POINT('Ctrl Pts',(-0.0018937522113587,0.161805701157652,
0.241028366254156));
#40214=CARTESIAN_POINT('Ctrl Pts',(-0.137121421381912,0.0859208183297427,
0.248980870369259));
#40215=CARTESIAN_POINT('Ctrl Pts',(-0.146432299282947,-0.0688640178244077,
0.256933374484361));
#40216=CARTESIAN_POINT('Ctrl Pts',(-0.0212763296414524,-0.160411935407873,
0.264885878599465));
#40217=CARTESIAN_POINT('Ctrl Pts',(0.123417412665197,-0.104655690124044,
0.272838382714567));
#40218=CARTESIAN_POINT('Ctrl Pts',(0.154778574015767,0.0472044939582724,
0.28079088682967));
#40219=CARTESIAN_POINT('Ctrl Pts',(0.0440086139068953,0.155717414331996,
0.288743390944773));
#40220=CARTESIAN_POINT('Ctrl Pts',(-0.107173875445849,0.121237088576372,
0.296695895059875));
#40221=CARTESIAN_POINT('Ctrl Pts',(-0.159940009655938,-0.0245736553055878,
0.304648399174979));
#40222=CARTESIAN_POINT('Ctrl Pts',(-0.0658353441931666,-0.147818735886772,
0.312600903290081));
#40223=CARTESIAN_POINT('Ctrl Pts',(0.0887250488340134,-0.135323822498093,
0.320553407405184));
#40224=CARTESIAN_POINT('Ctrl Pts',(0.161810400657075,0.00143717084316612,
0.328505911520287));
#40225=CARTESIAN_POINT('Ctrl Pts',(0.0863073974718863,0.136878429149436,
0.33645841563539));
#40226=CARTESIAN_POINT('Ctrl Pts',(-0.0684505496358049,0.146626032784815,
0.344410919750492));
#40227=CARTESIAN_POINT('Ctrl Pts',(-0.160351260416479,0.0217288858867957,
0.352363423865596));
#40228=CARTESIAN_POINT('Ctrl Pts',(-0.105003525631241,-0.123121609963769,
0.360315927980698));
#40229=CARTESIAN_POINT('Ctrl Pts',(0.0467675611965104,-0.154911156838423,
0.368268432095801));
#40230=CARTESIAN_POINT('Ctrl Pts',(0.155592612973961,-0.0444478326960028,
0.376220936210903));
#40231=CARTESIAN_POINT('Ctrl Pts',(0.121539023828006,0.106831348553276,
0.384173440326007));
#40232=CARTESIAN_POINT('Ctrl Pts',(-0.0241222499571812,0.160008714396091,
0.392125944441109));
#40233=CARTESIAN_POINT('Ctrl Pts',(-0.147632373634519,0.0662521864660413,
0.400078448556213));
#40234=CARTESIAN_POINT('Ctrl Pts',(-0.135573649464267,-0.0883428432395635,
0.408030952671315));
#40235=CARTESIAN_POINT('Ctrl Pts',(0.00098059051083778,-0.161813818534397,
0.415983456786418));
#40236=CARTESIAN_POINT('Ctrl Pts',(0.136634323339825,-0.0866932765836425,
0.423935960901521));
#40237=CARTESIAN_POINT('Ctrl Pts',(0.146818643894656,0.068036512042807,
0.431888465016623));
#40238=CARTESIAN_POINT('Ctrl Pts',(0.0221811834420201,0.160289355015634,
0.439840969131727));
#40239=CARTESIAN_POINT('Ctrl Pts',(-0.122824664094011,0.105350436989503,
0.447793473246828));
#40240=CARTESIAN_POINT('Ctrl Pts',(-0.155042815727352,-0.0463300886426471,
0.455745977361933));
#40241=CARTESIAN_POINT('Ctrl Pts',(-0.0448861093263465,-0.155466890947849,
0.463698481477034));
#40242=CARTESIAN_POINT('Ctrl Pts',(0.106486852993449,-0.121839386582653,
0.471650985592139));
#40243=CARTESIAN_POINT('Ctrl Pts',(0.160078270104732,0.0236695030909907,
0.47960348970724));
#40244=CARTESIAN_POINT('Ctrl Pts',(0.0666644623728171,0.147447020596393,
0.487555993822343));
#40245=CARTESIAN_POINT('Ctrl Pts',(-0.087952257620471,0.135818244448492,
0.495508497937446));
#40246=CARTESIAN_POINT('Ctrl Pts',(-0.161830540810569,-0.000516108099224624,
0.503461002052549));
#40247=CARTESIAN_POINT('Ctrl Pts',(-0.0870507091382164,-0.136404149983702,
0.511413506167652));
#40248=CARTESIAN_POINT('Ctrl Pts',(0.0675690001343951,-0.146981398376774,
0.519366010282755));
#40249=CARTESIAN_POINT('Ctrl Pts',(0.16032830198575,-0.0226890204033332,
0.527318514397857));
#40250=CARTESIAN_POINT('Ctrl Pts',(0.105489414021532,0.122642716620584,
0.53527101851296));
#40251=CARTESIAN_POINT('Ctrl Pts',(0.00490214493024879,0.144133374197726,
0.540572687923028));
#40252=CARTESIAN_POINT('Ctrl Pts',(-0.0388047044046456,0.131206995015769,
0.543223522628063));
#40253=CARTESIAN_POINT('Ctrl Pts',(-0.0634007094575211,0.131904027763685,
0.));
#40254=CARTESIAN_POINT('Ctrl Pts',(-0.107339749959441,0.110784382003547,
0.00265083470503427));
#40255=CARTESIAN_POINT('Ctrl Pts',(-0.171684059780304,0.0215447005535634,
0.00795250411510281));
#40256=CARTESIAN_POINT('Ctrl Pts',(-0.110860953190881,-0.133069336628884,
0.0159050082302056));
#40257=CARTESIAN_POINT('Ctrl Pts',(0.0519117226680141,-0.165059354817326,
0.0238575123453085));
#40258=CARTESIAN_POINT('Ctrl Pts',(0.166938819754359,-0.045692445844369,
0.0318100164604112));
#40259=CARTESIAN_POINT('Ctrl Pts',(0.128707834787806,0.11574507779797,0.0397625205755141));
#40260=CARTESIAN_POINT('Ctrl Pts',(-0.0277346835769849,0.170836721147544,
0.0477150246906169));
#40261=CARTESIAN_POINT('Ctrl Pts',(-0.158697852682494,0.0690821280092034,
0.0556675288057197));
#40262=CARTESIAN_POINT('Ctrl Pts',(-0.143936642246025,-0.0961259112316717,
0.0636200329208225));
#40263=CARTESIAN_POINT('Ctrl Pts',(0.00300271935518024,-0.173054250792614,
0.0715725370359253));
#40264=CARTESIAN_POINT('Ctrl Pts',(0.14718312786408,-0.0910736516165751,
0.0795250411510281));
#40265=CARTESIAN_POINT('Ctrl Pts',(0.156208052339,0.0745410449363381,0.0874775452661308));
#40266=CARTESIAN_POINT('Ctrl Pts',(0.0217887425894723,0.171704439392484,
0.0954300493812338));
#40267=CARTESIAN_POINT('Ctrl Pts',(-0.132638649479586,0.11119456839884,
0.103382553496337));
#40268=CARTESIAN_POINT('Ctrl Pts',(-0.165265842816907,-0.0514241515016591,
0.111335057611439));
#40269=CARTESIAN_POINT('Ctrl Pts',(-0.0461315298523219,-0.166820570613858,
0.119287561726542));
#40270=CARTESIAN_POINT('Ctrl Pts',(0.115364724197092,-0.129027957109734,
0.127240065841645));
#40271=CARTESIAN_POINT('Ctrl Pts',(0.170923092625556,0.0272493764316328,
0.135192569956748));
#40272=CARTESIAN_POINT('Ctrl Pts',(0.0695250318900354,0.158503940884133,
0.143145074071851));
#40273=CARTESIAN_POINT('Ctrl Pts',(-0.0957169429781459,0.144206442545789,
0.151097578186953));
#40274=CARTESIAN_POINT('Ctrl Pts',(-0.173063315155402,-0.00251393578307793,
0.159050082302056));
#40275=CARTESIAN_POINT('Ctrl Pts',(-0.0914879280754666,-0.146925796220795,
0.167002586417159));
#40276=CARTESIAN_POINT('Ctrl Pts',(0.0740996150085664,-0.156417639414764,
0.174955090532262));
#40277=CARTESIAN_POINT('Ctrl Pts',(0.171642460113959,-0.0222732279635641,
0.182907594647365));
#40278=CARTESIAN_POINT('Ctrl Pts',(0.111568299557575,0.132324394162615,
0.190860098762467));
#40279=CARTESIAN_POINT('Ctrl Pts',(-0.0509575576899273,0.165410272089882,
0.19881260287757));
#40280=CARTESIAN_POINT('Ctrl Pts',(-0.166689762399376,0.0466020803974948,
0.206765106992673));
#40281=CARTESIAN_POINT('Ctrl Pts',(-0.129352958553163,-0.115000186500534,
0.214717611107776));
#40282=CARTESIAN_POINT('Ctrl Pts',(0.0267669596738252,-0.170999300166548,
0.222670115222879));
#40283=CARTESIAN_POINT('Ctrl Pts',(0.15830713216098,-0.0699720136370574,
0.230622619337982));
#40284=CARTESIAN_POINT('Ctrl Pts',(0.144475954815417,0.0953096493813769,
0.238575123453084));
#40285=CARTESIAN_POINT('Ctrl Pts',(-0.00202558476983171,0.173069719454941,
0.246527627568187));
#40286=CARTESIAN_POINT('Ctrl Pts',(-0.146667056599619,0.091902150649062,
0.25448013168329));
#40287=CARTESIAN_POINT('Ctrl Pts',(-0.156626106340649,-0.073657949998918,
0.262432635798393));
#40288=CARTESIAN_POINT('Ctrl Pts',(-0.0227574700751082,-0.171578927439738,
0.270385139913495));
#40289=CARTESIAN_POINT('Ctrl Pts',(0.132009050564966,-0.111941240633319,
0.278337644028599));
#40290=CARTESIAN_POINT('Ctrl Pts',(0.165553402574146,0.0504906098358712,
0.286290148143701));
#40291=CARTESIAN_POINT('Ctrl Pts',(0.0470722502852127,0.16655759976238,
0.294242652258804));
#40292=CARTESIAN_POINT('Ctrl Pts',(-0.11463472809428,0.129676944368004,
0.302195156373907));
#40293=CARTESIAN_POINT('Ctrl Pts',(-0.171074148826212,-0.0262843373211962,
0.31014766048901));
#40294=CARTESIAN_POINT('Ctrl Pts',(-0.0704184368548879,-0.158109058995279,
0.318100164604112));
#40295=CARTESIAN_POINT('Ctrl Pts',(0.0949015961765597,-0.144744318820362,
0.326052668719215));
#40296=CARTESIAN_POINT('Ctrl Pts',(0.173074746107531,0.00153721873120606,
0.334005172834318));
#40297=CARTESIAN_POINT('Ctrl Pts',(0.0923156412937011,0.146407148591411,
0.341957676949421));
#40298=CARTESIAN_POINT('Ctrl Pts',(-0.0732156984410742,0.156833326497772,
0.349910181064524));
#40299=CARTESIAN_POINT('Ctrl Pts',(-0.171514028590913,0.0232415307840867,
0.357862685179626));
#40300=CARTESIAN_POINT('Ctrl Pts',(-0.112313290525359,-0.131692655714946,
0.365815189294729));
#40301=CARTESIAN_POINT('Ctrl Pts',(0.0500232602310192,-0.165695215079871,
0.373767693409832));
#40302=CARTESIAN_POINT('Ctrl Pts',(0.16642411042382,-0.0475420450579947,
0.381720197524935));
#40303=CARTESIAN_POINT('Ctrl Pts',(0.129999898682469,0.114268356373264,
0.389672701640038));
#40304=CARTESIAN_POINT('Ctrl Pts',(-0.0258015076282358,0.171147636410509,
0.39762520575514));
#40305=CARTESIAN_POINT('Ctrl Pts',(-0.157909723233413,0.0708642973820958,
0.405577709870244));
#40306=CARTESIAN_POINT('Ctrl Pts',(-0.145011537358637,-0.0944927835418238,
0.413530213985346));
#40307=CARTESIAN_POINT('Ctrl Pts',(0.00104885380055552,-0.173078401918574,
0.421482718100449));
#40308=CARTESIAN_POINT('Ctrl Pts',(0.146146049484986,-0.0927283831757074,
0.429435222215551));
#40309=CARTESIAN_POINT('Ctrl Pts',(0.157039346128141,0.0727728378400491,
0.437387726330655));
#40310=CARTESIAN_POINT('Ctrl Pts',(0.0237253147943705,0.171447813678334,
0.445340230445757));
#40311=CARTESIAN_POINT('Ctrl Pts',(-0.131375038115538,0.112684351934323,
0.45329273456086));
#40312=CARTESIAN_POINT('Ctrl Pts',(-0.16583603933271,-0.0495553332567244,
0.461245238675963));
#40313=CARTESIAN_POINT('Ctrl Pts',(-0.0480108320841284,-0.166289636325362,
0.469197742791066));
#40314=CARTESIAN_POINT('Ctrl Pts',(0.113899878937264,-0.130321171031401,
0.477150246906169));
#40315=CARTESIAN_POINT('Ctrl Pts',(0.171222034203015,0.0253172430284407,
0.485102751021271));
#40316=CARTESIAN_POINT('Ctrl Pts',(0.071305273658044,0.157711466941583,
0.493055255136374));
#40317=CARTESIAN_POINT('Ctrl Pts',(-0.0940750075114624,0.145273159693308,
0.501007759251477));
#40318=CARTESIAN_POINT('Ctrl Pts',(-0.173096288307157,-0.000552036691550711,
0.50896026336658));
#40319=CARTESIAN_POINT('Ctrl Pts',(-0.0931106982085004,-0.14589985273243,
0.516912767481683));
#40320=CARTESIAN_POINT('Ctrl Pts',(0.0722727803374284,-0.157213430677441,
0.524865271596785));
#40321=CARTESIAN_POINT('Ctrl Pts',(0.171489471921174,-0.0242685045571198,
0.532817775711888));
#40322=CARTESIAN_POINT('Ctrl Pts',(0.112833003778924,0.131180424464991,
0.540770279826991));
#40323=CARTESIAN_POINT('Ctrl Pts',(0.00524340515652838,0.154167142801661,
0.54607194923706));
#40324=CARTESIAN_POINT('Ctrl Pts',(-0.0415060733756244,0.140340900570494,
0.548722783942094));
#40325=CARTESIAN_POINT('Ctrl Pts',(-0.146267142220666,-0.000128791573925899,
0.458934495415709));
#40326=CARTESIAN_POINT('Ctrl Pts',(-0.146386413462202,-0.014310462982192,
0.459704743169127));
#40327=CARTESIAN_POINT('Ctrl Pts',(-0.144492166435918,-0.0284609503391585,
0.460474990922545));
#40328=CARTESIAN_POINT('Ctrl Pts',(-0.140455004588417,-0.04197110290299,
0.461245238675963));
#40329=CARTESIAN_POINT('Ctrl Pts',(-0.126560970249849,-0.0884667676129373,
0.463896073380997));
#40330=CARTESIAN_POINT('Ctrl Pts',(-0.0872859011669886,-0.12737820196915,
0.466546908086032));
#40331=CARTESIAN_POINT('Ctrl Pts',(-0.0406632481219932,-0.140839174931596,
0.469197742791066));
#40332=CARTESIAN_POINT('Ctrl Pts',(0.00595940492300207,-0.154300147894042,
0.4718485774961));
#40333=CARTESIAN_POINT('Ctrl Pts',(0.0599296419301325,-0.142310659462721,
0.474499412201135));
#40334=CARTESIAN_POINT('Ctrl Pts',(0.0964684529779897,-0.110376179570421,
0.477150246906169));
#40335=CARTESIAN_POINT('Ctrl Pts',(0.133007264025847,-0.0784416996781205,
0.479801081611203));
#40336=CARTESIAN_POINT('Ctrl Pts',(0.152114649114431,-0.0265622283248395,
0.482451916316237));
#40337=CARTESIAN_POINT('Ctrl Pts',(0.145015548234561,0.0214432113373248,
0.485102751021272));
#40338=CARTESIAN_POINT('Ctrl Pts',(0.137916447354691,0.0694486509994885,
0.487753585726306));
#40339=CARTESIAN_POINT('Ctrl Pts',(0.104610860506367,0.113580058970536,
0.49040442043134));
#40340=CARTESIAN_POINT('Ctrl Pts',(0.0603946868872881,0.133572711748014,
0.493055255136374));
#40341=CARTESIAN_POINT('Ctrl Pts',(0.0161785132682088,0.153565364525491,
0.495706089841409));
#40342=CARTESIAN_POINT('Ctrl Pts',(-0.0389482471216264,0.1494192621094,
0.498356924546443));
#40343=CARTESIAN_POINT('Ctrl Pts',(-0.0796818407824932,0.123042011503878,
0.501007759251477));
#40344=CARTESIAN_POINT('Ctrl Pts',(-0.0932156861533014,0.114278099486334,
0.501888506167652));
#40345=CARTESIAN_POINT('Ctrl Pts',(-0.105160643384876,0.103060050144818,
0.502769253083826));
#40346=CARTESIAN_POINT('Ctrl Pts',(-0.115072616245005,0.0902061753896192,
0.50365));
#40347=CARTESIAN_POINT('Ctrl Pts',(-0.0686153921261811,-0.0959615133978097,
-2.38524477946811E-18));
#40348=CARTESIAN_POINT('Ctrl Pts',(-0.0712073975642253,-0.0945517549303093,
-2.83889532725695E-18));
#40349=CARTESIAN_POINT('Ctrl Pts',(-0.0737377474651001,-0.0930410231931718,
5.14426139154652E-18));
#40350=CARTESIAN_POINT('Ctrl Pts',(-0.0761998018605363,-0.091430646244207,
6.50521303491303E-18));
#40351=CARTESIAN_POINT('Ctrl Pts',(-0.0821844297375259,-0.0875162295688071,
8.61254391956714E-18));
#40352=CARTESIAN_POINT('Ctrl Pts',(-0.0877662752922461,-0.0830147043174395,
8.93950144287772E-18));
#40353=CARTESIAN_POINT('Ctrl Pts',(-0.0929202787198591,-0.0780195924546499,
9.54097911787244E-18));
#40354=CARTESIAN_POINT('Ctrl Pts',(-0.0954786058604465,-0.0755401353824292,
9.83953861283751E-18));
#40355=CARTESIAN_POINT('Ctrl Pts',(-0.0979275180792717,-0.0729421130511386,
1.49939491249404E-17));
#40356=CARTESIAN_POINT('Ctrl Pts',(-0.100258897735172,-0.0702429236064683,
1.47451495458029E-17));
#40357=CARTESIAN_POINT('Ctrl Pts',(-0.104668940139426,-0.0651371314726185,
1.42745197659725E-17));
#40358=CARTESIAN_POINT('Ctrl Pts',(-0.108665118623842,-0.0596642636850333,
-1.289688799178E-17));
#40359=CARTESIAN_POINT('Ctrl Pts',(-0.112224391688578,-0.0538945629536488,
-2.42861286636753E-17));
#40360=CARTESIAN_POINT('Ctrl Pts',(-0.114007263482302,-0.0510044681210456,
-2.99911014422584E-17));
#40361=CARTESIAN_POINT('Ctrl Pts',(-0.115680198610802,-0.0480392113919056,
-9.85233076388881E-18));
#40362=CARTESIAN_POINT('Ctrl Pts',(-0.117233217251657,-0.0450208645520303,
-8.67361737988404E-18));
#40363=CARTESIAN_POINT('Ctrl Pts',(-0.121574823694362,-0.0365827983617143,
-5.37841570781424E-18));
#40364=CARTESIAN_POINT('Ctrl Pts',(-0.124997594823754,-0.027708690332575,
-9.37762199309504E-19));
#40365=CARTESIAN_POINT('Ctrl Pts',(-0.127437485841812,-0.018577962661637,
9.54097911787244E-18));
#40366=CARTESIAN_POINT('Ctrl Pts',(-0.12867484687016,-0.0139474252741679,
1.48551452162951E-17));
#40367=CARTESIAN_POINT('Ctrl Pts',(-0.129658851279119,-0.00925026145395888,
3.85592351303264E-18));
#40368=CARTESIAN_POINT('Ctrl Pts',(-0.13037677319566,-0.00450727571206391,
1.12757025938492E-17));
#40369=CARTESIAN_POINT('Ctrl Pts',(-0.130820878643177,-0.00157327166937493,
1.5865567080829E-17));
#40370=CARTESIAN_POINT('Ctrl Pts',(-0.131161668086746,0.00136911314303839,
-1.28026844144678E-17));
#40371=CARTESIAN_POINT('Ctrl Pts',(-0.131397381290232,0.00431340779322604,
-1.38777878078145E-17));
#40372=CARTESIAN_POINT('Ctrl Pts',(-0.131719489313798,0.0083368605168951,
-1.53469436465178E-17));
#40373=CARTESIAN_POINT('Ctrl Pts',(-0.131845540542961,0.0123645321806217,
2.00482317967995E-17));
#40374=CARTESIAN_POINT('Ctrl Pts',(-0.131770346471732,0.0163834363085182,
1.56125112837913E-17));
#40375=CARTESIAN_POINT('Ctrl Pts',(-0.131648667841181,0.0228868047604438,
8.25177748690449E-18));
#40376=CARTESIAN_POINT('Ctrl Pts',(-0.131000732502959,0.0293672129596454,
8.03096099599679E-18));
#40377=CARTESIAN_POINT('Ctrl Pts',(-0.129864039936534,0.0357832484813204,
1.04083408558608E-17));
#40378=CARTESIAN_POINT('Ctrl Pts',(-0.129251059617937,0.0392432020469336,
1.16903823743602E-17));
#40379=CARTESIAN_POINT('Ctrl Pts',(-0.128495732458156,0.0426844698916631,
9.6775998731851E-18));
#40380=CARTESIAN_POINT('Ctrl Pts',(-0.127602533865954,0.0461005734698996,
1.21430643318376E-17));
#40381=CARTESIAN_POINT('Ctrl Pts',(-0.126801717254801,0.0491633553806105,
1.43535300781251E-17));
#40382=CARTESIAN_POINT('Ctrl Pts',(-0.125892295195939,0.0521970927094408,
-2.04303423409802E-17));
#40383=CARTESIAN_POINT('Ctrl Pts',(-0.12487995022281,0.0551944839930744,
-1.90819582357449E-17));
#40384=CARTESIAN_POINT('Ctrl Pts',(-0.122213990144214,0.063087964688102,
-1.55310558352899E-17));
#40385=CARTESIAN_POINT('Ctrl Pts',(-0.118834573434494,0.0707355529753685,
-2.09602125306395E-19));
#40386=CARTESIAN_POINT('Ctrl Pts',(-0.114813287039476,0.0780547614149283,
-3.46944695195361E-18));
#40387=CARTESIAN_POINT('Ctrl Pts',(-0.112113271799503,0.0829691028445349,
-5.65820692756715E-18));
#40388=CARTESIAN_POINT('Ctrl Pts',(-0.109123295952561,0.0877354841888059,
1.59792597750096E-17));
#40389=CARTESIAN_POINT('Ctrl Pts',(-0.105858764968584,0.0923275350572008,
1.73472347597681E-17));
#40390=CARTESIAN_POINT('Ctrl Pts',(-0.104035851863276,0.0948917348608856,
1.81111115738308E-17));
#40391=CARTESIAN_POINT('Ctrl Pts',(-0.102127627911009,0.0974005222622627,
-1.86461934882118E-17));
#40392=CARTESIAN_POINT('Ctrl Pts',(-0.100145200306236,0.0998394990060757,
-1.56125112837913E-17));
#40393=CARTESIAN_POINT('Ctrl Pts',(-0.0936292563097381,0.10785605196023,
-5.64125013933619E-18));
#40394=CARTESIAN_POINT('Ctrl Pts',(-0.0862946795456802,0.115149852779714,
-9.28670353986392E-18));
#40395=CARTESIAN_POINT('Ctrl Pts',(-0.0782486257709069,0.121568627915854,
-1.38777878078145E-17));
#40396=CARTESIAN_POINT('Ctrl Pts',(-0.0735390572914751,0.125325707088318,
-1.65650710848099E-17));
#40397=CARTESIAN_POINT('Ctrl Pts',(-0.0685847970970084,0.128782722422648,
6.71820819248872E-19));
#40398=CARTESIAN_POINT('Ctrl Pts',(-0.0634007094575211,0.131904027763685,
0.));
#40399=CARTESIAN_POINT('Origin',(0.,0.,0.));
#40400=CARTESIAN_POINT('Origin',(-0.0577350269189626,-0.1,-0.3));
#40401=CARTESIAN_POINT('',(-0.0577350269189626,-0.1,-0.3));
#40402=CARTESIAN_POINT('',(0.0577350269189626,-0.1,-0.3));
#40403=CARTESIAN_POINT('',(-0.0288675134594813,-0.1,-0.3));
#40404=CARTESIAN_POINT('',(-0.0577350269189626,-0.1,-0.1));
#40405=CARTESIAN_POINT('',(-0.0577350269189626,-0.1,-0.3));
#40406=CARTESIAN_POINT('',(0.0577350269189626,-0.1,-0.1));
#40407=CARTESIAN_POINT('',(-0.0577350269189626,-0.1,-0.1));
#40408=CARTESIAN_POINT('',(0.0577350269189626,-0.1,-0.3));
#40409=CARTESIAN_POINT('Origin',(-0.115470053837925,1.41410031829988E-17,
-0.3));
#40410=CARTESIAN_POINT('',(-0.115470053837925,1.41410031829988E-17,-0.3));
#40411=CARTESIAN_POINT('',(-0.101036297108185,-0.025,-0.3));
#40412=CARTESIAN_POINT('',(-0.115470053837925,1.38777878078145E-17,-0.1));
#40413=CARTESIAN_POINT('',(-0.115470053837925,1.41410031829988E-17,-0.3));
#40414=CARTESIAN_POINT('',(-0.115470053837925,1.41410031829988E-17,-0.1));
#40415=CARTESIAN_POINT('Origin',(-0.0577350269189626,0.1,-0.3));
#40416=CARTESIAN_POINT('',(-0.0577350269189626,0.1,-0.3));
#40417=CARTESIAN_POINT('',(-0.0721687836487032,0.075,-0.3));
#40418=CARTESIAN_POINT('',(-0.0577350269189626,0.1,-0.1));
#40419=CARTESIAN_POINT('',(-0.0577350269189626,0.1,-0.3));
#40420=CARTESIAN_POINT('',(-0.0577350269189626,0.1,-0.1));
#40421=CARTESIAN_POINT('Origin',(0.0577350269189626,0.1,-0.3));
#40422=CARTESIAN_POINT('',(0.0577350269189626,0.1,-0.3));
#40423=CARTESIAN_POINT('',(0.0288675134594813,0.1,-0.3));
#40424=CARTESIAN_POINT('',(0.0577350269189626,0.1,-0.1));
#40425=CARTESIAN_POINT('',(0.0577350269189626,0.1,-0.3));
#40426=CARTESIAN_POINT('',(0.0577350269189626,0.1,-0.1));
#40427=CARTESIAN_POINT('Origin',(0.115470053837925,0.,-0.3));
#40428=CARTESIAN_POINT('',(0.115470053837925,0.,-0.3));
#40429=CARTESIAN_POINT('',(0.101036297108185,0.025,-0.3));
#40430=CARTESIAN_POINT('',(0.115470053837925,0.,-0.1));
#40431=CARTESIAN_POINT('',(0.115470053837925,0.,-0.3));
#40432=CARTESIAN_POINT('',(0.115470053837925,0.,-0.1));
#40433=CARTESIAN_POINT('Origin',(0.0577350269189626,-0.1,-0.3));
#40434=CARTESIAN_POINT('',(0.0721687836487032,-0.075,-0.3));
#40435=CARTESIAN_POINT('',(0.0577350269189626,-0.1,-0.1));
#40436=CARTESIAN_POINT('Origin',(0.,0.,-0.1));
#40437=CARTESIAN_POINT('Origin',(0.,0.,0.));
#40438=CARTESIAN_POINT('',(-0.3,-3.67394039744206E-17,0.));
#40439=CARTESIAN_POINT('Origin',(0.,0.,0.));
#40440=CARTESIAN_POINT('Origin',(0.,0.,-0.3));
#40441=CARTESIAN_POINT('',(-0.3,-3.67394039744206E-17,-0.3));
#40442=CARTESIAN_POINT('',(-0.3,-3.67394039744206E-17,-0.3));
#40443=CARTESIAN_POINT('Origin',(0.,0.,-0.3));
#40444=CARTESIAN_POINT('Origin',(0.,0.,-0.3));
#40445=CARTESIAN_POINT('Origin',(0.,0.,0.6));
#43958=UNCERTAINTY_MEASURE_WITH_UNIT(LENGTH_MEASURE(0.001),#43981,
'DISTANCE_ACCURACY_VALUE',
'Maximum model space distance between geometric entities at asserted c
onnectivities');
#43961=UNCERTAINTY_MEASURE_WITH_UNIT(LENGTH_MEASURE(0.001),#43981,
'DISTANCE_ACCURACY_VALUE',
'Maximum model space distance between geometric entities at asserted c
onnectivities');
#43977=(
GEOMETRIC_REPRESENTATION_CONTEXT(3)
GLOBAL_UNCERTAINTY_ASSIGNED_CONTEXT((#43958))
GLOBAL_UNIT_ASSIGNED_CONTEXT((#43981,#43983,#43984))
REPRESENTATION_CONTEXT('','3D')
);
#43980=(
GEOMETRIC_REPRESENTATION_CONTEXT(3)
GLOBAL_UNCERTAINTY_ASSIGNED_CONTEXT((#43961))
GLOBAL_UNIT_ASSIGNED_CONTEXT((#43981,#43983,#43984))
REPRESENTATION_CONTEXT('','3D')
);
#43981=(
LENGTH_UNIT()
NAMED_UNIT(*)
SI_UNIT(.CENTI.,.METRE.)
);
#43983=(
NAMED_UNIT(*)
PLANE_ANGLE_UNIT()
SI_UNIT($,.RADIAN.)
);
#43984=(
NAMED_UNIT(*)
SI_UNIT($,.STERADIAN.)
SOLID_ANGLE_UNIT()
);
#44000=SHAPE_DEFINITION_REPRESENTATION(#44018,#44070);
#44018=PRODUCT_DEFINITION_SHAPE('',$,#44089);
#44070=SHAPE_REPRESENTATION('',(#12107),#43977);
#44073=PRODUCT_DEFINITION_CONTEXT('part definition',#44129,'design');
#44089=PRODUCT_DEFINITION('Socket head cap screw M3x6',
'Socket head cap screw M3x6',#44107,#44073);
#44107=PRODUCT_DEFINITION_FORMATION('',$,#44146);
#44129=APPLICATION_CONTEXT(
'Core Data for Automotive Mechanical Design Process');
#44130=PRODUCT_CONTEXT('part definition',#44129,'mechanical');
#44146=PRODUCT('Socket head cap screw M3x6',
'Socket head cap screw M3x6',$,(#44130));
#44160=PRESENTATION_STYLE_ASSIGNMENT((#44172));
#44172=SURFACE_STYLE_USAGE(.BOTH.,#44184);
#44184=SURFACE_SIDE_STYLE('',(#44196));
#44196=SURFACE_STYLE_FILL_AREA(#44208);
#44208=FILL_AREA_STYLE('Dark gray',(#44220));
#44220=FILL_AREA_STYLE_COLOUR('Dark gray',#44232);
#44232=COLOUR_RGB('Dark gray',0.250980392156863,0.282352941176471,0.32156862745098);
ENDSEC;
END-ISO-10303-21;
